ISO-10303-21;
HEADER;
/* Generated by software containing ST-Developer
 * from STEP Tools, Inc. (www.steptools.com) 
 */

FILE_DESCRIPTION(
/* description */ (''),
/* implementation_level */ '2;1');

FILE_NAME(
/* name */ 'CarregeSupport.step',
/* time_stamp */ '2026-10-05T11:01:41-07:00',
/* author */ (''),
/* organization */ (''),
/* preprocessor_version */ 'ST-DEVELOPER v20.2',
/* originating_system */ 'Autodesk Translation Framework v15.15.0.0',
/* authorisation */ '');

FILE_SCHEMA (('AUTOMOTIVE_DESIGN { 1 0 10303 214 3 1 1 }'));
ENDSEC;

DATA;
#10=MECHANICAL_DESIGN_GEOMETRIC_PRESENTATION_REPRESENTATION('',(#2140),#215609);
#47=SPHERICAL_SURFACE('',#28803,0.5);
#48=SPHERICAL_SURFACE('',#28805,0.5);
#49=SPHERICAL_SURFACE('',#28844,0.5);
#50=SPHERICAL_SURFACE('',#28850,0.5);
#55=(
BOUNDED_SURFACE()
B_SPLINE_SURFACE(2,2,((#124503,#124504,#124505),(#124506,#124507,#124508),
(#124509,#124510,#124511)),.UNSPECIFIED.,.F.,.F.,.F.)
B_SPLINE_SURFACE_WITH_KNOTS((3,3),(3,3),(-1.57079632679498,3.62708052714211E-14),
(-3.14159265358979,-1.57079632679461),.UNSPECIFIED.)
GEOMETRIC_REPRESENTATION_ITEM()
RATIONAL_B_SPLINE_SURFACE(((1.,0.707106781186447,1.),(0.707106781186491,
0.499999999999889,0.707106781186491),(1.,0.707106781186447,1.)))
REPRESENTATION_ITEM('')
SURFACE()
);
#56=(
BOUNDED_SURFACE()
B_SPLINE_SURFACE(2,2,((#124580,#124581,#124582),(#124583,#124584,#124585),
(#124586,#124587,#124588)),.UNSPECIFIED.,.F.,.F.,.F.)
B_SPLINE_SURFACE_WITH_KNOTS((3,3),(3,3),(-1.57079632679491,8.49689085742031E-14),
(-1.57076063039803,3.56963973534065E-5),.UNSPECIFIED.)
GEOMETRIC_REPRESENTATION_ITEM()
RATIONAL_B_SPLINE_SURFACE(((1.,0.707106781186375,1.),(0.707106781186495,
0.499999999999841,0.707106781186495),(1.,0.707106781186375,1.)))
REPRESENTATION_ITEM('')
SURFACE()
);
#57=(
BOUNDED_SURFACE()
B_SPLINE_SURFACE(2,2,((#124901,#124902,#124903),(#124904,#124905,#124906),
(#124907,#124908,#124909)),.UNSPECIFIED.,.F.,.F.,.F.)
B_SPLINE_SURFACE_WITH_KNOTS((3,3),(3,3),(-9.79900252594829E-15,1.57079632679518),
(-1.57076063039766,3.56963969770062E-5),.UNSPECIFIED.)
GEOMETRIC_REPRESENTATION_ITEM()
RATIONAL_B_SPLINE_SURFACE(((1.,0.707106781186639,1.),(0.70710678118645,
0.499999999999996,0.70710678118645),(1.,0.707106781186639,1.)))
REPRESENTATION_ITEM('')
SURFACE()
);
#58=(
BOUNDED_SURFACE()
B_SPLINE_SURFACE(2,2,((#124959,#124960,#124961),(#124962,#124963,#124964),
(#124965,#124966,#124967)),.UNSPECIFIED.,.F.,.F.,.F.)
B_SPLINE_SURFACE_WITH_KNOTS((3,3),(3,3),(-7.03247557642951E-14,1.57079632679488),
(-3.14159265358978,-1.57079632679492),.UNSPECIFIED.)
GEOMETRIC_REPRESENTATION_ITEM()
RATIONAL_B_SPLINE_SURFACE(((1.,0.707106781186562,1.),(0.707106781186541,
0.500000000000006,0.707106781186541),(1.,0.707106781186562,1.)))
REPRESENTATION_ITEM('')
SURFACE()
);
#63=TOROIDAL_SURFACE('',#28727,1.008,0.5);
#64=TOROIDAL_SURFACE('',#28733,2.5,0.5);
#65=TOROIDAL_SURFACE('',#28739,4.5,0.5);
#66=TOROIDAL_SURFACE('',#28754,1.49999999999999,0.5);
#67=TOROIDAL_SURFACE('',#28763,1.5,0.5);
#68=TOROIDAL_SURFACE('',#28778,4.5,0.5);
#69=TOROIDAL_SURFACE('',#28784,2.5,0.5);
#70=TOROIDAL_SURFACE('',#28790,1.008,0.5);
#71=TOROIDAL_SURFACE('',#28834,3.5,0.5);
#72=TOROIDAL_SURFACE('',#28845,3.5,0.5);
#73=TOROIDAL_SURFACE('',#28865,2.5,0.5);
#74=TOROIDAL_SURFACE('',#28873,4.5,0.5);
#75=TOROIDAL_SURFACE('',#28874,2.5,0.5);
#76=TOROIDAL_SURFACE('',#28880,1.5,0.5);
#77=TOROIDAL_SURFACE('',#28892,1.49999999999999,0.5);
#78=TOROIDAL_SURFACE('',#28898,4.5,0.5);
#95=ELLIPSE('',#28721,0.51530681467495,0.5);
#96=ELLIPSE('',#28749,0.541196100146195,0.5);
#97=ELLIPSE('',#28751,0.541196100146199,0.5);
#98=ELLIPSE('',#28759,0.515306814674945,0.5);
#99=ELLIPSE('',#28768,0.541196100146198,0.5);
#100=ELLIPSE('',#28770,0.541196100146195,0.5);
#101=ELLIPSE('',#28869,0.541196100146197,0.5);
#102=ELLIPSE('',#28876,0.541196100146196,0.5);
#103=ELLIPSE('',#28879,0.51530681467495,0.5);
#104=ELLIPSE('',#28885,0.515306814674951,0.5);
#105=ELLIPSE('',#28891,0.541196100146195,0.5);
#106=ELLIPSE('',#28897,0.541196100146198,0.5);
#200=FACE_BOUND('',#4764,.T.);
#201=FACE_BOUND('',#4819,.T.);
#1143=B_SPLINE_CURVE_WITH_KNOTS('',3,(#124743,#124744,#124745,#124746,#124747,
#124748,#124749,#124750,#124751,#124752,#124753,#124754,#124755,#124756),
 .UNSPECIFIED.,.F.,.F.,(4,2,2,2,2,2,4),(-0.179602182967889,-0.179256977579304,
-0.171704143510179,-0.143638027894992,-0.121065001388227,-0.103941692121038,
-0.0932595456500115),.UNSPECIFIED.);
#1144=B_SPLINE_CURVE_WITH_KNOTS('',3,(#124761,#124762,#124763,#124764,#124765,
#124766,#124767,#124768),.UNSPECIFIED.,.F.,.F.,(4,2,2,4),(-0.000485046858822211,
0.,0.0275595172389922,0.0494496501685093),.UNSPECIFIED.);
#1145=B_SPLINE_CURVE_WITH_KNOTS('',3,(#124769,#124770,#124771,#124772,#124773,
#124774,#124775,#124776,#124777,#124778,#124779,#124780),.UNSPECIFIED.,
 .F.,.F.,(4,2,2,2,2,4),(0.0518378816079573,0.0543463464547439,0.0792065654069019,
0.0971521945631999,0.111639541304113,0.114326698243711),.UNSPECIFIED.);
#1146=B_SPLINE_CURVE_WITH_KNOTS('',3,(#124801,#124802,#124803,#124804,#124805,
#124806,#124807,#124808,#124809,#124810,#124811,#124812),.UNSPECIFIED.,
 .F.,.F.,(4,2,2,2,2,4),(0.129817017894095,0.133096428805707,0.150776811474232,
0.172677687900067,0.203017141504491,0.206078476281295),.UNSPECIFIED.);
#1147=B_SPLINE_CURVE_WITH_KNOTS('',3,(#124814,#124815,#124816,#124817,#124818,
#124819,#124820,#124821),.UNSPECIFIED.,.F.,.F.,(4,2,2,4),(0.195623656529068,
0.221185285948212,0.253367190411721,0.253933591177603),.UNSPECIFIED.);
#1148=B_SPLINE_CURVE_WITH_KNOTS('',3,(#124824,#124825,#124826,#124827,#124828,
#124829,#124830,#124831,#124832,#124833,#124834,#124835,#124836,#124837),
 .UNSPECIFIED.,.F.,.F.,(4,2,2,2,2,2,4),(-0.000415314508934373,0.,0.00908676885214763,
0.0428529422959233,0.0700104135552468,0.0906113630623747,0.103462988682372),
 .UNSPECIFIED.);
#2122=SHAPE_REPRESENTATION_RELATIONSHIP('SRR','None',#215648,#2131);
#2131=ADVANCED_BREP_SHAPE_REPRESENTATION('',(#2149),#215604);
#2140=STYLED_ITEM('',(#215698),#2149);
#2149=MANIFOLD_SOLID_BREP('Body1',#28083);
#2448=CYLINDRICAL_SURFACE('',#28711,3.);
#2449=CYLINDRICAL_SURFACE('',#28715,3.);
#2450=CYLINDRICAL_SURFACE('',#28719,0.5);
#2451=CYLINDRICAL_SURFACE('',#28722,0.5);
#2452=CYLINDRICAL_SURFACE('',#28724,0.5);
#2453=CYLINDRICAL_SURFACE('',#28731,0.5);
#2454=CYLINDRICAL_SURFACE('',#28737,0.5);
#2455=CYLINDRICAL_SURFACE('',#28743,0.5);
#2456=CYLINDRICAL_SURFACE('',#28748,0.5);
#2457=CYLINDRICAL_SURFACE('',#28750,0.5);
#2458=CYLINDRICAL_SURFACE('',#28752,0.5);
#2459=CYLINDRICAL_SURFACE('',#28758,0.5);
#2460=CYLINDRICAL_SURFACE('',#28760,0.5);
#2461=CYLINDRICAL_SURFACE('',#28761,0.5);
#2462=CYLINDRICAL_SURFACE('',#28767,0.5);
#2463=CYLINDRICAL_SURFACE('',#28769,0.5);
#2464=CYLINDRICAL_SURFACE('',#28771,0.5);
#2465=CYLINDRICAL_SURFACE('',#28776,0.5);
#2466=CYLINDRICAL_SURFACE('',#28782,0.5);
#2467=CYLINDRICAL_SURFACE('',#28788,0.5);
#2468=CYLINDRICAL_SURFACE('',#28794,0.5);
#2469=CYLINDRICAL_SURFACE('',#28796,0.5);
#2470=CYLINDRICAL_SURFACE('',#28799,0.5);
#2471=CYLINDRICAL_SURFACE('',#28801,0.5);
#2472=CYLINDRICAL_SURFACE('',#28808,1.);
#2473=CYLINDRICAL_SURFACE('',#28813,1.);
#2474=CYLINDRICAL_SURFACE('',#28816,5.);
#2475=CYLINDRICAL_SURFACE('',#28819,3.);
#2476=CYLINDRICAL_SURFACE('',#28823,0.508000000000002);
#2477=CYLINDRICAL_SURFACE('',#28826,0.5);
#2478=CYLINDRICAL_SURFACE('',#28832,0.5);
#2479=CYLINDRICAL_SURFACE('',#28837,0.5);
#2480=CYLINDRICAL_SURFACE('',#28840,0.5);
#2481=CYLINDRICAL_SURFACE('',#28842,0.5);
#2482=CYLINDRICAL_SURFACE('',#28848,0.5);
#2483=CYLINDRICAL_SURFACE('',#28852,0.5);
#2484=CYLINDRICAL_SURFACE('',#28862,0.5);
#2485=CYLINDRICAL_SURFACE('',#28867,0.5);
#2486=CYLINDRICAL_SURFACE('',#28871,0.5);
#2487=CYLINDRICAL_SURFACE('',#28875,0.5);
#2488=CYLINDRICAL_SURFACE('',#28877,0.5);
#2489=CYLINDRICAL_SURFACE('',#28882,0.5);
#2490=CYLINDRICAL_SURFACE('',#28883,0.5);
#2491=CYLINDRICAL_SURFACE('',#28886,0.5);
#2492=CYLINDRICAL_SURFACE('',#28888,0.5);
#2493=CYLINDRICAL_SURFACE('',#28889,0.5);
#2494=CYLINDRICAL_SURFACE('',#28895,0.5);
#2495=CYLINDRICAL_SURFACE('',#28896,0.5);
#2496=CYLINDRICAL_SURFACE('',#28901,0.5);
#2497=CYLINDRICAL_SURFACE('',#28905,0.5);
#2498=CYLINDRICAL_SURFACE('',#28910,0.999999999999992);
#2499=CYLINDRICAL_SURFACE('',#28914,1.);
#2500=CYLINDRICAL_SURFACE('',#28916,5.);
#2501=CYLINDRICAL_SURFACE('',#28918,3.);
#2502=CYLINDRICAL_SURFACE('',#28920,3.);
#2503=CYLINDRICAL_SURFACE('',#28922,3.);
#2504=CYLINDRICAL_SURFACE('',#28928,0.508000000000002);
#2505=CYLINDRICAL_SURFACE('',#28930,0.499999999999998);
#3379=FACE_OUTER_BOUND('',#4719,.T.);
#3380=FACE_OUTER_BOUND('',#4720,.T.);
#3381=FACE_OUTER_BOUND('',#4721,.T.);
#3382=FACE_OUTER_BOUND('',#4722,.T.);
#3383=FACE_OUTER_BOUND('',#4723,.T.);
#3384=FACE_OUTER_BOUND('',#4724,.T.);
#3385=FACE_OUTER_BOUND('',#4725,.T.);
#3386=FACE_OUTER_BOUND('',#4726,.T.);
#3387=FACE_OUTER_BOUND('',#4727,.T.);
#3388=FACE_OUTER_BOUND('',#4728,.T.);
#3389=FACE_OUTER_BOUND('',#4729,.T.);
#3390=FACE_OUTER_BOUND('',#4730,.T.);
#3391=FACE_OUTER_BOUND('',#4731,.T.);
#3392=FACE_OUTER_BOUND('',#4732,.T.);
#3393=FACE_OUTER_BOUND('',#4733,.T.);
#3394=FACE_OUTER_BOUND('',#4734,.T.);
#3395=FACE_OUTER_BOUND('',#4735,.T.);
#3396=FACE_OUTER_BOUND('',#4736,.T.);
#3397=FACE_OUTER_BOUND('',#4737,.T.);
#3398=FACE_OUTER_BOUND('',#4738,.T.);
#3399=FACE_OUTER_BOUND('',#4739,.T.);
#3400=FACE_OUTER_BOUND('',#4740,.T.);
#3401=FACE_OUTER_BOUND('',#4741,.T.);
#3402=FACE_OUTER_BOUND('',#4742,.T.);
#3403=FACE_OUTER_BOUND('',#4743,.T.);
#3404=FACE_OUTER_BOUND('',#4744,.T.);
#3405=FACE_OUTER_BOUND('',#4745,.T.);
#3406=FACE_OUTER_BOUND('',#4746,.T.);
#3407=FACE_OUTER_BOUND('',#4747,.T.);
#3408=FACE_OUTER_BOUND('',#4748,.T.);
#3409=FACE_OUTER_BOUND('',#4749,.T.);
#3410=FACE_OUTER_BOUND('',#4750,.T.);
#3411=FACE_OUTER_BOUND('',#4751,.T.);
#3412=FACE_OUTER_BOUND('',#4752,.T.);
#3413=FACE_OUTER_BOUND('',#4753,.T.);
#3414=FACE_OUTER_BOUND('',#4754,.T.);
#3415=FACE_OUTER_BOUND('',#4755,.T.);
#3416=FACE_OUTER_BOUND('',#4756,.T.);
#3417=FACE_OUTER_BOUND('',#4757,.T.);
#3418=FACE_OUTER_BOUND('',#4758,.T.);
#3419=FACE_OUTER_BOUND('',#4759,.T.);
#3420=FACE_OUTER_BOUND('',#4760,.T.);
#3421=FACE_OUTER_BOUND('',#4761,.T.);
#3422=FACE_OUTER_BOUND('',#4762,.T.);
#3423=FACE_OUTER_BOUND('',#4763,.T.);
#3424=FACE_OUTER_BOUND('',#4765,.T.);
#3425=FACE_OUTER_BOUND('',#4766,.T.);
#3426=FACE_OUTER_BOUND('',#4767,.T.);
#3427=FACE_OUTER_BOUND('',#4768,.T.);
#3428=FACE_OUTER_BOUND('',#4769,.T.);
#3429=FACE_OUTER_BOUND('',#4770,.T.);
#3430=FACE_OUTER_BOUND('',#4771,.T.);
#3431=FACE_OUTER_BOUND('',#4772,.T.);
#3432=FACE_OUTER_BOUND('',#4773,.T.);
#3433=FACE_OUTER_BOUND('',#4774,.T.);
#3434=FACE_OUTER_BOUND('',#4775,.T.);
#3435=FACE_OUTER_BOUND('',#4776,.T.);
#3436=FACE_OUTER_BOUND('',#4777,.T.);
#3437=FACE_OUTER_BOUND('',#4778,.T.);
#3438=FACE_OUTER_BOUND('',#4779,.T.);
#3439=FACE_OUTER_BOUND('',#4780,.T.);
#3440=FACE_OUTER_BOUND('',#4781,.T.);
#3441=FACE_OUTER_BOUND('',#4782,.T.);
#3442=FACE_OUTER_BOUND('',#4783,.T.);
#3443=FACE_OUTER_BOUND('',#4784,.T.);
#3444=FACE_OUTER_BOUND('',#4785,.T.);
#3445=FACE_OUTER_BOUND('',#4786,.T.);
#3446=FACE_OUTER_BOUND('',#4787,.T.);
#3447=FACE_OUTER_BOUND('',#4788,.T.);
#3448=FACE_OUTER_BOUND('',#4789,.T.);
#3449=FACE_OUTER_BOUND('',#4790,.T.);
#3450=FACE_OUTER_BOUND('',#4791,.T.);
#3451=FACE_OUTER_BOUND('',#4792,.T.);
#3452=FACE_OUTER_BOUND('',#4793,.T.);
#3453=FACE_OUTER_BOUND('',#4794,.T.);
#3454=FACE_OUTER_BOUND('',#4795,.T.);
#3455=FACE_OUTER_BOUND('',#4796,.T.);
#3456=FACE_OUTER_BOUND('',#4797,.T.);
#3457=FACE_OUTER_BOUND('',#4798,.T.);
#3458=FACE_OUTER_BOUND('',#4799,.T.);
#3459=FACE_OUTER_BOUND('',#4800,.T.);
#3460=FACE_OUTER_BOUND('',#4801,.T.);
#3461=FACE_OUTER_BOUND('',#4802,.T.);
#3462=FACE_OUTER_BOUND('',#4803,.T.);
#3463=FACE_OUTER_BOUND('',#4804,.T.);
#3464=FACE_OUTER_BOUND('',#4805,.T.);
#3465=FACE_OUTER_BOUND('',#4806,.T.);
#3466=FACE_OUTER_BOUND('',#4807,.T.);
#3467=FACE_OUTER_BOUND('',#4808,.T.);
#3468=FACE_OUTER_BOUND('',#4809,.T.);
#3469=FACE_OUTER_BOUND('',#4810,.T.);
#3470=FACE_OUTER_BOUND('',#4811,.T.);
#3471=FACE_OUTER_BOUND('',#4812,.T.);
#3472=FACE_OUTER_BOUND('',#4813,.T.);
#3473=FACE_OUTER_BOUND('',#4814,.T.);
#3474=FACE_OUTER_BOUND('',#4815,.T.);
#3475=FACE_OUTER_BOUND('',#4816,.T.);
#3476=FACE_OUTER_BOUND('',#4817,.T.);
#3477=FACE_OUTER_BOUND('',#4818,.T.);
#3478=FACE_OUTER_BOUND('',#4820,.T.);
#3479=FACE_OUTER_BOUND('',#4821,.T.);
#3480=FACE_OUTER_BOUND('',#4822,.T.);
#3481=FACE_OUTER_BOUND('',#4823,.T.);
#3482=FACE_OUTER_BOUND('',#4824,.T.);
#3483=FACE_OUTER_BOUND('',#4825,.T.);
#3484=FACE_OUTER_BOUND('',#4826,.T.);
#3485=FACE_OUTER_BOUND('',#4827,.T.);
#3486=FACE_OUTER_BOUND('',#4828,.T.);
#3487=FACE_OUTER_BOUND('',#4829,.T.);
#3488=FACE_OUTER_BOUND('',#4830,.T.);
#4719=EDGE_LOOP('',(#20641,#20642,#20643,#20644));
#4720=EDGE_LOOP('',(#20645));
#4721=EDGE_LOOP('',(#20646,#20647,#20648,#20649));
#4722=EDGE_LOOP('',(#20650));
#4723=EDGE_LOOP('',(#20651,#20652,#20653,#20654));
#4724=EDGE_LOOP('',(#20655,#20656,#20657,#20658));
#4725=EDGE_LOOP('',(#20659,#20660,#20661,#20662));
#4726=EDGE_LOOP('',(#20663,#20664,#20665,#20666));
#4727=EDGE_LOOP('',(#20667,#20668,#20669,#20670));
#4728=EDGE_LOOP('',(#20671,#20672,#20673,#20674));
#4729=EDGE_LOOP('',(#20675,#20676,#20677,#20678));
#4730=EDGE_LOOP('',(#20679,#20680,#20681,#20682));
#4731=EDGE_LOOP('',(#20683,#20684,#20685,#20686));
#4732=EDGE_LOOP('',(#20687,#20688,#20689,#20690));
#4733=EDGE_LOOP('',(#20691,#20692,#20693,#20694));
#4734=EDGE_LOOP('',(#20695,#20696,#20697,#20698));
#4735=EDGE_LOOP('',(#20699,#20700,#20701,#20702));
#4736=EDGE_LOOP('',(#20703,#20704,#20705,#20706));
#4737=EDGE_LOOP('',(#20707,#20708,#20709,#20710));
#4738=EDGE_LOOP('',(#20711,#20712,#20713,#20714));
#4739=EDGE_LOOP('',(#20715,#20716,#20717,#20718));
#4740=EDGE_LOOP('',(#20719,#20720,#20721,#20722));
#4741=EDGE_LOOP('',(#20723,#20724,#20725,#20726));
#4742=EDGE_LOOP('',(#20727,#20728,#20729,#20730));
#4743=EDGE_LOOP('',(#20731,#20732,#20733,#20734));
#4744=EDGE_LOOP('',(#20735,#20736,#20737,#20738));
#4745=EDGE_LOOP('',(#20739,#20740,#20741,#20742));
#4746=EDGE_LOOP('',(#20743,#20744,#20745,#20746));
#4747=EDGE_LOOP('',(#20747,#20748,#20749,#20750));
#4748=EDGE_LOOP('',(#20751,#20752,#20753,#20754));
#4749=EDGE_LOOP('',(#20755,#20756,#20757,#20758));
#4750=EDGE_LOOP('',(#20759,#20760,#20761,#20762));
#4751=EDGE_LOOP('',(#20763,#20764,#20765,#20766));
#4752=EDGE_LOOP('',(#20767,#20768,#20769,#20770));
#4753=EDGE_LOOP('',(#20771,#20772,#20773,#20774));
#4754=EDGE_LOOP('',(#20775,#20776,#20777,#20778));
#4755=EDGE_LOOP('',(#20779,#20780,#20781));
#4756=EDGE_LOOP('',(#20782,#20783,#20784));
#4757=EDGE_LOOP('',(#20785,#20786,#20787,#20788));
#4758=EDGE_LOOP('',(#20789,#20790,#20791,#20792));
#4759=EDGE_LOOP('',(#20793,#20794,#20795,#20796));
#4760=EDGE_LOOP('',(#20797,#20798,#20799,#20800));
#4761=EDGE_LOOP('',(#20801,#20802,#20803,#20804));
#4762=EDGE_LOOP('',(#20805,#20806,#20807,#20808));
#4763=EDGE_LOOP('',(#20809,#20810,#20811,#20812));
#4764=EDGE_LOOP('',(#20813));
#4765=EDGE_LOOP('',(#20814,#20815,#20816,#20817));
#4766=EDGE_LOOP('',(#20818,#20819,#20820,#20821));
#4767=EDGE_LOOP('',(#20822,#20823,#20824,#20825,#20826,#20827));
#4768=EDGE_LOOP('',(#20828,#20829,#20830,#20831));
#4769=EDGE_LOOP('',(#20832,#20833,#20834,#20835));
#4770=EDGE_LOOP('',(#20836,#20837,#20838,#20839,#20840,#20841));
#4771=EDGE_LOOP('',(#20842,#20843,#20844,#20845));
#4772=EDGE_LOOP('',(#20846,#20847,#20848,#20849));
#4773=EDGE_LOOP('',(#20850,#20851,#20852,#20853));
#4774=EDGE_LOOP('',(#20854,#20855,#20856,#20857));
#4775=EDGE_LOOP('',(#20858,#20859,#20860,#20861,#20862,#20863,#20864,#20865,
#20866,#20867,#20868,#20869,#20870,#20871,#20872,#20873,#20874,#20875,#20876,
#20877,#20878,#20879,#20880,#20881,#20882,#20883,#20884,#20885,#20886,#20887,
#20888,#20889));
#4776=EDGE_LOOP('',(#20890,#20891,#20892,#20893));
#4777=EDGE_LOOP('',(#20894,#20895,#20896,#20897,#20898));
#4778=EDGE_LOOP('',(#20899,#20900,#20901,#20902));
#4779=EDGE_LOOP('',(#20903,#20904,#20905,#20906));
#4780=EDGE_LOOP('',(#20907,#20908,#20909,#20910));
#4781=EDGE_LOOP('',(#20911,#20912,#20913));
#4782=EDGE_LOOP('',(#20914,#20915,#20916,#20917,#20918));
#4783=EDGE_LOOP('',(#20919,#20920,#20921,#20922));
#4784=EDGE_LOOP('',(#20923,#20924,#20925));
#4785=EDGE_LOOP('',(#20926,#20927,#20928,#20929,#20930));
#4786=EDGE_LOOP('',(#20931,#20932,#20933,#20934,#20935,#20936,#20937,#20938,
#20939,#20940,#20941,#20942,#20943,#20944,#20945,#20946,#20947,#20948,#20949,
#20950,#20951,#20952,#20953,#20954,#20955,#20956,#20957,#20958));
#4787=EDGE_LOOP('',(#20959,#20960,#20961,#20962,#20963));
#4788=EDGE_LOOP('',(#20964,#20965,#20966));
#4789=EDGE_LOOP('',(#20967,#20968,#20969,#20970));
#4790=EDGE_LOOP('',(#20971,#20972,#20973,#20974));
#4791=EDGE_LOOP('',(#20975,#20976,#20977,#20978));
#4792=EDGE_LOOP('',(#20979,#20980,#20981,#20982));
#4793=EDGE_LOOP('',(#20983,#20984,#20985));
#4794=EDGE_LOOP('',(#20986,#20987,#20988,#20989));
#4795=EDGE_LOOP('',(#20990,#20991,#20992,#20993));
#4796=EDGE_LOOP('',(#20994,#20995,#20996,#20997));
#4797=EDGE_LOOP('',(#20998,#20999,#21000,#21001));
#4798=EDGE_LOOP('',(#21002,#21003,#21004,#21005));
#4799=EDGE_LOOP('',(#21006,#21007,#21008,#21009));
#4800=EDGE_LOOP('',(#21010,#21011,#21012,#21013));
#4801=EDGE_LOOP('',(#21014,#21015,#21016,#21017));
#4802=EDGE_LOOP('',(#21018,#21019,#21020,#21021));
#4803=EDGE_LOOP('',(#21022,#21023,#21024,#21025));
#4804=EDGE_LOOP('',(#21026,#21027,#21028,#21029));
#4805=EDGE_LOOP('',(#21030,#21031,#21032,#21033));
#4806=EDGE_LOOP('',(#21034,#21035,#21036,#21037));
#4807=EDGE_LOOP('',(#21038,#21039,#21040,#21041));
#4808=EDGE_LOOP('',(#21042,#21043,#21044,#21045));
#4809=EDGE_LOOP('',(#21046,#21047,#21048,#21049));
#4810=EDGE_LOOP('',(#21050,#21051,#21052,#21053));
#4811=EDGE_LOOP('',(#21054,#21055,#21056,#21057));
#4812=EDGE_LOOP('',(#21058,#21059,#21060,#21061));
#4813=EDGE_LOOP('',(#21062,#21063,#21064,#21065));
#4814=EDGE_LOOP('',(#21066,#21067,#21068,#21069));
#4815=EDGE_LOOP('',(#21070,#21071,#21072,#21073));
#4816=EDGE_LOOP('',(#21074,#21075,#21076,#21077));
#4817=EDGE_LOOP('',(#21078,#21079,#21080,#21081));
#4818=EDGE_LOOP('',(#21082,#21083,#21084,#21085));
#4819=EDGE_LOOP('',(#21086));
#4820=EDGE_LOOP('',(#21087,#21088,#21089,#21090));
#4821=EDGE_LOOP('',(#21091,#21092,#21093,#21094));
#4822=EDGE_LOOP('',(#21095,#21096,#21097,#21098,#21099,#21100));
#4823=EDGE_LOOP('',(#21101,#21102,#21103,#21104));
#4824=EDGE_LOOP('',(#21105,#21106,#21107,#21108));
#4825=EDGE_LOOP('',(#21109,#21110,#21111,#21112,#21113));
#4826=EDGE_LOOP('',(#21114,#21115,#21116,#21117,#21118));
#4827=EDGE_LOOP('',(#21119,#21120,#21121,#21122));
#4828=EDGE_LOOP('',(#21123,#21124,#21125,#21126));
#4829=EDGE_LOOP('',(#21127,#21128,#21129,#21130,#21131,#21132));
#4830=EDGE_LOOP('',(#21133,#21134,#21135,#21136));
#5788=CIRCLE('',#28712,3.);
#5789=CIRCLE('',#28713,3.);
#5790=CIRCLE('',#28716,3.);
#5791=CIRCLE('',#28717,3.);
#5792=CIRCLE('',#28720,0.499999999999998);
#5793=CIRCLE('',#28723,0.499999999999999);
#5794=CIRCLE('',#28725,0.5);
#5795=CIRCLE('',#28726,0.499999999999998);
#5796=CIRCLE('',#28728,0.499999999999998);
#5797=CIRCLE('',#28729,0.508000000000002);
#5798=CIRCLE('',#28730,1.008);
#5799=CIRCLE('',#28732,0.499999999999998);
#5800=CIRCLE('',#28734,0.499999999999998);
#5801=CIRCLE('',#28735,3.);
#5802=CIRCLE('',#28736,2.5);
#5803=CIRCLE('',#28738,0.499999999999998);
#5804=CIRCLE('',#28740,0.499999999999998);
#5805=CIRCLE('',#28741,5.);
#5806=CIRCLE('',#28742,4.5);
#5807=CIRCLE('',#28744,0.499999999999998);
#5808=CIRCLE('',#28745,0.499999999999998);
#5809=CIRCLE('',#28746,1.);
#5810=CIRCLE('',#28747,0.500000000000001);
#5811=CIRCLE('',#28753,0.499999999999998);
#5812=CIRCLE('',#28755,0.499999999999998);
#5813=CIRCLE('',#28756,0.999999999999992);
#5814=CIRCLE('',#28757,1.49999999999999);
#5815=CIRCLE('',#28762,0.499999999999998);
#5816=CIRCLE('',#28764,0.499999999999998);
#5817=CIRCLE('',#28765,1.);
#5818=CIRCLE('',#28766,1.5);
#5819=CIRCLE('',#28772,0.499999999999998);
#5820=CIRCLE('',#28773,0.499999999999998);
#5821=CIRCLE('',#28774,1.);
#5822=CIRCLE('',#28775,0.5);
#5823=CIRCLE('',#28777,0.499999999999998);
#5824=CIRCLE('',#28779,0.499999999999998);
#5825=CIRCLE('',#28780,5.);
#5826=CIRCLE('',#28781,4.5);
#5827=CIRCLE('',#28783,0.499999999999998);
#5828=CIRCLE('',#28785,0.499999999999998);
#5829=CIRCLE('',#28786,3.);
#5830=CIRCLE('',#28787,2.5);
#5831=CIRCLE('',#28789,0.499999999999998);
#5832=CIRCLE('',#28791,0.499999999999998);
#5833=CIRCLE('',#28792,0.508000000000002);
#5834=CIRCLE('',#28793,1.008);
#5835=CIRCLE('',#28795,0.499999999999998);
#5836=CIRCLE('',#28797,0.499999999999998);
#5837=CIRCLE('',#28798,0.499999999999998);
#5838=CIRCLE('',#28800,0.500000000000004);
#5839=CIRCLE('',#28802,0.499999999999993);
#5840=CIRCLE('',#28804,0.5);
#5841=CIRCLE('',#28806,0.499999999999998);
#5842=CIRCLE('',#28809,1.);
#5843=CIRCLE('',#28814,1.);
#5844=CIRCLE('',#28817,5.);
#5845=CIRCLE('',#28820,3.);
#5846=CIRCLE('',#28821,3.);
#5847=CIRCLE('',#28824,0.508000000000002);
#5848=CIRCLE('',#28827,0.5);
#5849=CIRCLE('',#28833,0.5);
#5850=CIRCLE('',#28835,3.5);
#5851=CIRCLE('',#28836,3.);
#5852=CIRCLE('',#28838,0.500000000000002);
#5853=CIRCLE('',#28839,0.5);
#5854=CIRCLE('',#28841,0.500000000000004);
#5855=CIRCLE('',#28843,0.499999999999998);
#5856=CIRCLE('',#28846,3.);
#5857=CIRCLE('',#28847,3.5);
#5858=CIRCLE('',#28849,0.5);
#5859=CIRCLE('',#28851,0.499999999999998);
#5860=CIRCLE('',#28853,0.499999999999998);
#5861=CIRCLE('',#28854,0.500000000000001);
#5862=CIRCLE('',#28856,4.5);
#5863=CIRCLE('',#28857,0.500000000000001);
#5864=CIRCLE('',#28858,1.49999999999999);
#5865=CIRCLE('',#28859,1.5);
#5866=CIRCLE('',#28860,0.5);
#5867=CIRCLE('',#28861,4.5);
#5868=CIRCLE('',#28863,0.499999999999999);
#5869=CIRCLE('',#28864,0.499999999999999);
#5870=CIRCLE('',#28866,3.);
#5871=CIRCLE('',#28868,0.5);
#5872=CIRCLE('',#28870,0.500000000000002);
#5873=CIRCLE('',#28872,0.499999999999998);
#5874=CIRCLE('',#28878,0.499999999999995);
#5875=CIRCLE('',#28881,0.5);
#5876=CIRCLE('',#28884,0.499999999999998);
#5877=CIRCLE('',#28887,0.499999999999999);
#5878=CIRCLE('',#28890,0.5);
#5879=CIRCLE('',#28893,0.500000000000001);
#5880=CIRCLE('',#28894,0.999999999999992);
#5881=CIRCLE('',#28899,0.499999999999998);
#5882=CIRCLE('',#28900,5.);
#5883=CIRCLE('',#28902,0.499999999999998);
#5884=CIRCLE('',#28903,0.5);
#5885=CIRCLE('',#28904,1.);
#5886=CIRCLE('',#28919,3.);
#5887=CIRCLE('',#28921,3.);
#5888=CIRCLE('',#28923,3.);
#5889=CIRCLE('',#28926,0.508000000000002);
#6832=LINE('',#124433,#8677);
#6833=LINE('',#124440,#8678);
#6834=LINE('',#124446,#8679);
#6835=LINE('',#124450,#8680);
#6836=LINE('',#124454,#8681);
#6837=LINE('',#124457,#8682);
#6838=LINE('',#124463,#8683);
#6839=LINE('',#124466,#8684);
#6840=LINE('',#124477,#8685);
#6841=LINE('',#124478,#8686);
#6842=LINE('',#124489,#8687);
#6843=LINE('',#124490,#8688);
#6844=LINE('',#124501,#8689);
#6845=LINE('',#124502,#8690);
#6846=LINE('',#124519,#8691);
#6847=LINE('',#124521,#8692);
#6848=LINE('',#124525,#8693);
#6849=LINE('',#124527,#8694);
#6850=LINE('',#124531,#8695);
#6851=LINE('',#124534,#8696);
#6852=LINE('',#124543,#8697);
#6853=LINE('',#124545,#8698);
#6854=LINE('',#124548,#8699);
#6855=LINE('',#124549,#8700);
#6856=LINE('',#124552,#8701);
#6857=LINE('',#124555,#8702);
#6858=LINE('',#124564,#8703);
#6859=LINE('',#124566,#8704);
#6860=LINE('',#124570,#8705);
#6861=LINE('',#124573,#8706);
#6862=LINE('',#124576,#8707);
#6863=LINE('',#124579,#8708);
#6864=LINE('',#124598,#8709);
#6865=LINE('',#124599,#8710);
#6866=LINE('',#124610,#8711);
#6867=LINE('',#124611,#8712);
#6868=LINE('',#124622,#8713);
#6869=LINE('',#124623,#8714);
#6870=LINE('',#124634,#8715);
#6871=LINE('',#124635,#8716);
#6872=LINE('',#124640,#8717);
#6873=LINE('',#124643,#8718);
#6874=LINE('',#124646,#8719);
#6875=LINE('',#124649,#8720);
#6876=LINE('',#124652,#8721);
#6877=LINE('',#124654,#8722);
#6878=LINE('',#124661,#8723);
#6879=LINE('',#124663,#8724);
#6880=LINE('',#124664,#8725);
#6881=LINE('',#124667,#8726);
#6882=LINE('',#124671,#8727);
#6883=LINE('',#124672,#8728);
#6884=LINE('',#124675,#8729);
#6885=LINE('',#124676,#8730);
#6886=LINE('',#124679,#8731);
#6887=LINE('',#124680,#8732);
#6888=LINE('',#124683,#8733);
#6889=LINE('',#124687,#8734);
#6890=LINE('',#124688,#8735);
#6891=LINE('',#124691,#8736);
#6892=LINE('',#124695,#8737);
#6893=LINE('',#124696,#8738);
#6894=LINE('',#124699,#8739);
#6895=LINE('',#124703,#8740);
#6896=LINE('',#124707,#8741);
#6897=LINE('',#124708,#8742);
#6898=LINE('',#124711,#8743);
#6899=LINE('',#124715,#8744);
#6900=LINE('',#124717,#8745);
#6901=LINE('',#124719,#8746);
#6902=LINE('',#124720,#8747);
#6903=LINE('',#124723,#8748);
#6904=LINE('',#124727,#8749);
#6905=LINE('',#124728,#8750);
#6906=LINE('',#124731,#8751);
#6907=LINE('',#124732,#8752);
#6908=LINE('',#124735,#8753);
#6909=LINE('',#124736,#8754);
#6910=LINE('',#124742,#8755);
#6911=LINE('',#124785,#8756);
#6912=LINE('',#124790,#8757);
#6913=LINE('',#124794,#8758);
#6914=LINE('',#124839,#8759);
#6915=LINE('',#124842,#8760);
#6916=LINE('',#124847,#8761);
#6917=LINE('',#124852,#8762);
#6918=LINE('',#124856,#8763);
#6919=LINE('',#124860,#8764);
#6920=LINE('',#124862,#8765);
#6921=LINE('',#124864,#8766);
#6922=LINE('',#124868,#8767);
#6923=LINE('',#124870,#8768);
#6924=LINE('',#124872,#8769);
#6925=LINE('',#124874,#8770);
#6926=LINE('',#124876,#8771);
#6927=LINE('',#124880,#8772);
#6928=LINE('',#124882,#8773);
#6929=LINE('',#124884,#8774);
#6930=LINE('',#124888,#8775);
#6931=LINE('',#124894,#8776);
#6932=LINE('',#124926,#8777);
#6933=LINE('',#124932,#8778);
#6934=LINE('',#124934,#8779);
#6935=LINE('',#124938,#8780);
#6936=LINE('',#124946,#8781);
#6937=LINE('',#124949,#8782);
#6938=LINE('',#124958,#8783);
#6939=LINE('',#124972,#8784);
#6940=LINE('',#124974,#8785);
#6941=LINE('',#124976,#8786);
#6942=LINE('',#124978,#8787);
#6943=LINE('',#124980,#8788);
#6944=LINE('',#124982,#8789);
#6945=LINE('',#124984,#8790);
#6946=LINE('',#124986,#8791);
#6947=LINE('',#124988,#8792);
#6948=LINE('',#124990,#8793);
#6949=LINE('',#124992,#8794);
#6950=LINE('',#124994,#8795);
#6951=LINE('',#124996,#8796);
#6952=LINE('',#124999,#8797);
#6953=LINE('',#125002,#8798);
#6954=LINE('',#125005,#8799);
#6955=LINE('',#125012,#8800);
#6956=LINE('',#125014,#8801);
#6957=LINE('',#125017,#8802);
#6958=LINE('',#125019,#8803);
#6959=LINE('',#125021,#8804);
#8677=VECTOR('',#31770,3.);
#8678=VECTOR('',#31779,3.);
#8679=VECTOR('',#31786,10.);
#8680=VECTOR('',#31789,10.);
#8681=VECTOR('',#31794,10.);
#8682=VECTOR('',#31797,10.);
#8683=VECTOR('',#31802,10.);
#8684=VECTOR('',#31805,10.);
#8685=VECTOR('',#31818,10.);
#8686=VECTOR('',#31819,10.);
#8687=VECTOR('',#31832,10.);
#8688=VECTOR('',#31833,10.);
#8689=VECTOR('',#31846,10.);
#8690=VECTOR('',#31847,10.);
#8691=VECTOR('',#31856,10.);
#8692=VECTOR('',#31857,10.);
#8693=VECTOR('',#31862,10.);
#8694=VECTOR('',#31863,10.);
#8695=VECTOR('',#31868,10.);
#8696=VECTOR('',#31871,10.);
#8697=VECTOR('',#31882,10.);
#8698=VECTOR('',#31883,10.);
#8699=VECTOR('',#31888,10.);
#8700=VECTOR('',#31889,10.);
#8701=VECTOR('',#31892,10.);
#8702=VECTOR('',#31895,10.);
#8703=VECTOR('',#31906,10.);
#8704=VECTOR('',#31907,10.);
#8705=VECTOR('',#31912,10.);
#8706=VECTOR('',#31915,10.);
#8707=VECTOR('',#31918,10.);
#8708=VECTOR('',#31921,10.);
#8709=VECTOR('',#31932,10.);
#8710=VECTOR('',#31933,10.);
#8711=VECTOR('',#31946,10.);
#8712=VECTOR('',#31947,10.);
#8713=VECTOR('',#31960,10.);
#8714=VECTOR('',#31961,10.);
#8715=VECTOR('',#31974,10.);
#8716=VECTOR('',#31975,10.);
#8717=VECTOR('',#31980,10.);
#8718=VECTOR('',#31983,10.);
#8719=VECTOR('',#31986,10.);
#8720=VECTOR('',#31989,10.);
#8721=VECTOR('',#31992,10.);
#8722=VECTOR('',#31995,10.);
#8723=VECTOR('',#32006,10.);
#8724=VECTOR('',#32007,10.);
#8725=VECTOR('',#32008,10.);
#8726=VECTOR('',#32011,10.);
#8727=VECTOR('',#32016,10.);
#8728=VECTOR('',#32017,10.);
#8729=VECTOR('',#32020,10.);
#8730=VECTOR('',#32021,10.);
#8731=VECTOR('',#32024,10.);
#8732=VECTOR('',#32025,10.);
#8733=VECTOR('',#32028,10.);
#8734=VECTOR('',#32033,10.);
#8735=VECTOR('',#32034,10.);
#8736=VECTOR('',#32037,10.);
#8737=VECTOR('',#32042,10.);
#8738=VECTOR('',#32043,10.);
#8739=VECTOR('',#32046,10.);
#8740=VECTOR('',#32049,10.);
#8741=VECTOR('',#32054,10.);
#8742=VECTOR('',#32055,10.);
#8743=VECTOR('',#32058,10.);
#8744=VECTOR('',#32063,10.);
#8745=VECTOR('',#32064,10.);
#8746=VECTOR('',#32065,10.);
#8747=VECTOR('',#32066,10.);
#8748=VECTOR('',#32069,10.);
#8749=VECTOR('',#32074,10.);
#8750=VECTOR('',#32075,10.);
#8751=VECTOR('',#32078,10.);
#8752=VECTOR('',#32079,10.);
#8753=VECTOR('',#32082,10.);
#8754=VECTOR('',#32083,10.);
#8755=VECTOR('',#32090,10.);
#8756=VECTOR('',#32101,10.);
#8757=VECTOR('',#32108,10.);
#8758=VECTOR('',#32113,10.);
#8759=VECTOR('',#32124,10.);
#8760=VECTOR('',#32127,10.);
#8761=VECTOR('',#32134,10.);
#8762=VECTOR('',#32141,10.);
#8763=VECTOR('',#32144,10.);
#8764=VECTOR('',#32147,10.);
#8765=VECTOR('',#32148,10.);
#8766=VECTOR('',#32149,10.);
#8767=VECTOR('',#32152,10.);
#8768=VECTOR('',#32153,10.);
#8769=VECTOR('',#32154,10.);
#8770=VECTOR('',#32155,10.);
#8771=VECTOR('',#32156,10.);
#8772=VECTOR('',#32159,10.);
#8773=VECTOR('',#32160,10.);
#8774=VECTOR('',#32161,10.);
#8775=VECTOR('',#32164,10.);
#8776=VECTOR('',#32171,10.);
#8777=VECTOR('',#32212,10.);
#8778=VECTOR('',#32221,10.);
#8779=VECTOR('',#32224,10.);
#8780=VECTOR('',#32227,10.);
#8781=VECTOR('',#32240,10.);
#8782=VECTOR('',#32243,10.);
#8783=VECTOR('',#32256,10.);
#8784=VECTOR('',#32263,10.);
#8785=VECTOR('',#32266,10.);
#8786=VECTOR('',#32269,10.);
#8787=VECTOR('',#32272,10.);
#8788=VECTOR('',#32275,10.);
#8789=VECTOR('',#32278,10.);
#8790=VECTOR('',#32281,10.);
#8791=VECTOR('',#32284,10.);
#8792=VECTOR('',#32287,10.);
#8793=VECTOR('',#32290,10.);
#8794=VECTOR('',#32293,10.);
#8795=VECTOR('',#32296,10.);
#8796=VECTOR('',#32299,10.);
#8797=VECTOR('',#32302,10.);
#8798=VECTOR('',#32305,10.);
#8799=VECTOR('',#32308,10.);
#8800=VECTOR('',#32319,10.);
#8801=VECTOR('',#32320,10.);
#8802=VECTOR('',#32325,10.);
#8803=VECTOR('',#32328,10.);
#8804=VECTOR('',#32331,10.);
#11152=VERTEX_POINT('',#124430);
#11153=VERTEX_POINT('',#124432);
#11154=VERTEX_POINT('',#124437);
#11155=VERTEX_POINT('',#124439);
#11156=VERTEX_POINT('',#124444);
#11157=VERTEX_POINT('',#124445);
#11158=VERTEX_POINT('',#124447);
#11159=VERTEX_POINT('',#124449);
#11160=VERTEX_POINT('',#124453);
#11161=VERTEX_POINT('',#124455);
#11162=VERTEX_POINT('',#124459);
#11163=VERTEX_POINT('',#124460);
#11164=VERTEX_POINT('',#124462);
#11165=VERTEX_POINT('',#124464);
#11166=VERTEX_POINT('',#124468);
#11167=VERTEX_POINT('',#124469);
#11168=VERTEX_POINT('',#124474);
#11169=VERTEX_POINT('',#124475);
#11170=VERTEX_POINT('',#124480);
#11171=VERTEX_POINT('',#124481);
#11172=VERTEX_POINT('',#124486);
#11173=VERTEX_POINT('',#124487);
#11174=VERTEX_POINT('',#124492);
#11175=VERTEX_POINT('',#124493);
#11176=VERTEX_POINT('',#124498);
#11177=VERTEX_POINT('',#124499);
#11178=VERTEX_POINT('',#124512);
#11179=VERTEX_POINT('',#124513);
#11180=VERTEX_POINT('',#124518);
#11181=VERTEX_POINT('',#124520);
#11182=VERTEX_POINT('',#124524);
#11183=VERTEX_POINT('',#124526);
#11184=VERTEX_POINT('',#124530);
#11185=VERTEX_POINT('',#124532);
#11186=VERTEX_POINT('',#124536);
#11187=VERTEX_POINT('',#124537);
#11188=VERTEX_POINT('',#124542);
#11189=VERTEX_POINT('',#124544);
#11190=VERTEX_POINT('',#124551);
#11191=VERTEX_POINT('',#124553);
#11192=VERTEX_POINT('',#124557);
#11193=VERTEX_POINT('',#124558);
#11194=VERTEX_POINT('',#124563);
#11195=VERTEX_POINT('',#124565);
#11196=VERTEX_POINT('',#124569);
#11197=VERTEX_POINT('',#124571);
#11198=VERTEX_POINT('',#124575);
#11199=VERTEX_POINT('',#124577);
#11200=VERTEX_POINT('',#124589);
#11201=VERTEX_POINT('',#124590);
#11202=VERTEX_POINT('',#124595);
#11203=VERTEX_POINT('',#124596);
#11204=VERTEX_POINT('',#124601);
#11205=VERTEX_POINT('',#124602);
#11206=VERTEX_POINT('',#124607);
#11207=VERTEX_POINT('',#124608);
#11208=VERTEX_POINT('',#124613);
#11209=VERTEX_POINT('',#124614);
#11210=VERTEX_POINT('',#124619);
#11211=VERTEX_POINT('',#124620);
#11212=VERTEX_POINT('',#124625);
#11213=VERTEX_POINT('',#124626);
#11214=VERTEX_POINT('',#124631);
#11215=VERTEX_POINT('',#124632);
#11216=VERTEX_POINT('',#124637);
#11217=VERTEX_POINT('',#124638);
#11218=VERTEX_POINT('',#124641);
#11219=VERTEX_POINT('',#124645);
#11220=VERTEX_POINT('',#124647);
#11221=VERTEX_POINT('',#124651);
#11222=VERTEX_POINT('',#124660);
#11223=VERTEX_POINT('',#124662);
#11224=VERTEX_POINT('',#124666);
#11225=VERTEX_POINT('',#124670);
#11226=VERTEX_POINT('',#124674);
#11227=VERTEX_POINT('',#124678);
#11228=VERTEX_POINT('',#124682);
#11229=VERTEX_POINT('',#124686);
#11230=VERTEX_POINT('',#124690);
#11231=VERTEX_POINT('',#124694);
#11232=VERTEX_POINT('',#124698);
#11233=VERTEX_POINT('',#124700);
#11234=VERTEX_POINT('',#124702);
#11235=VERTEX_POINT('',#124706);
#11236=VERTEX_POINT('',#124710);
#11237=VERTEX_POINT('',#124714);
#11238=VERTEX_POINT('',#124716);
#11239=VERTEX_POINT('',#124718);
#11240=VERTEX_POINT('',#124722);
#11241=VERTEX_POINT('',#124726);
#11242=VERTEX_POINT('',#124730);
#11243=VERTEX_POINT('',#124734);
#11244=VERTEX_POINT('',#124739);
#11245=VERTEX_POINT('',#124741);
#11246=VERTEX_POINT('',#124758);
#11247=VERTEX_POINT('',#124760);
#11248=VERTEX_POINT('',#124783);
#11249=VERTEX_POINT('',#124788);
#11250=VERTEX_POINT('',#124792);
#11251=VERTEX_POINT('',#124797);
#11252=VERTEX_POINT('',#124798);
#11253=VERTEX_POINT('',#124800);
#11254=VERTEX_POINT('',#124813);
#11255=VERTEX_POINT('',#124822);
#11256=VERTEX_POINT('',#124840);
#11257=VERTEX_POINT('',#124846);
#11258=VERTEX_POINT('',#124851);
#11259=VERTEX_POINT('',#124853);
#11260=VERTEX_POINT('',#124855);
#11261=VERTEX_POINT('',#124857);
#11262=VERTEX_POINT('',#124859);
#11263=VERTEX_POINT('',#124861);
#11264=VERTEX_POINT('',#124863);
#11265=VERTEX_POINT('',#124865);
#11266=VERTEX_POINT('',#124867);
#11267=VERTEX_POINT('',#124869);
#11268=VERTEX_POINT('',#124871);
#11269=VERTEX_POINT('',#124873);
#11270=VERTEX_POINT('',#124875);
#11271=VERTEX_POINT('',#124877);
#11272=VERTEX_POINT('',#124879);
#11273=VERTEX_POINT('',#124881);
#11274=VERTEX_POINT('',#124883);
#11275=VERTEX_POINT('',#124885);
#11276=VERTEX_POINT('',#124887);
#11277=VERTEX_POINT('',#124891);
#11278=VERTEX_POINT('',#124893);
#11279=VERTEX_POINT('',#124924);
#11280=VERTEX_POINT('',#124925);
#11281=VERTEX_POINT('',#124930);
#11282=VERTEX_POINT('',#124936);
#11283=VERTEX_POINT('',#124937);
#11284=VERTEX_POINT('',#124942);
#11285=VERTEX_POINT('',#124948);
#11286=VERTEX_POINT('',#124952);
#11287=VERTEX_POINT('',#124956);
#11288=VERTEX_POINT('',#124968);
#11289=VERTEX_POINT('',#124998);
#11290=VERTEX_POINT('',#125000);
#11291=VERTEX_POINT('',#125004);
#11292=VERTEX_POINT('',#125011);
#11293=VERTEX_POINT('',#125013);
#14682=EDGE_CURVE('',#11152,#11152,#5788,.T.);
#14683=EDGE_CURVE('',#11152,#11153,#6832,.T.);
#14684=EDGE_CURVE('',#11153,#11153,#5789,.T.);
#14685=EDGE_CURVE('',#11154,#11154,#5790,.T.);
#14686=EDGE_CURVE('',#11154,#11155,#6833,.T.);
#14687=EDGE_CURVE('',#11155,#11155,#5791,.T.);
#14688=EDGE_CURVE('',#11156,#11157,#6834,.T.);
#14689=EDGE_CURVE('',#11157,#11158,#5792,.T.);
#14690=EDGE_CURVE('',#11158,#11159,#6835,.T.);
#14691=EDGE_CURVE('',#11159,#11156,#95,.T.);
#14692=EDGE_CURVE('',#11157,#11160,#6836,.T.);
#14693=EDGE_CURVE('',#11160,#11161,#5793,.T.);
#14694=EDGE_CURVE('',#11161,#11158,#6837,.T.);
#14695=EDGE_CURVE('',#11162,#11163,#5794,.T.);
#14696=EDGE_CURVE('',#11163,#11164,#6838,.T.);
#14697=EDGE_CURVE('',#11164,#11165,#5795,.T.);
#14698=EDGE_CURVE('',#11165,#11162,#6839,.T.);
#14699=EDGE_CURVE('',#11166,#11167,#5796,.T.);
#14700=EDGE_CURVE('',#11167,#11165,#5797,.T.);
#14701=EDGE_CURVE('',#11164,#11166,#5798,.T.);
#14702=EDGE_CURVE('',#11168,#11169,#5799,.T.);
#14703=EDGE_CURVE('',#11169,#11167,#6840,.T.);
#14704=EDGE_CURVE('',#11166,#11168,#6841,.T.);
#14705=EDGE_CURVE('',#11170,#11171,#5800,.T.);
#14706=EDGE_CURVE('',#11171,#11169,#5801,.T.);
#14707=EDGE_CURVE('',#11168,#11170,#5802,.T.);
#14708=EDGE_CURVE('',#11172,#11173,#5803,.T.);
#14709=EDGE_CURVE('',#11173,#11171,#6842,.T.);
#14710=EDGE_CURVE('',#11170,#11172,#6843,.T.);
#14711=EDGE_CURVE('',#11174,#11175,#5804,.T.);
#14712=EDGE_CURVE('',#11175,#11173,#5805,.T.);
#14713=EDGE_CURVE('',#11172,#11174,#5806,.T.);
#14714=EDGE_CURVE('',#11176,#11177,#5807,.T.);
#14715=EDGE_CURVE('',#11177,#11175,#6844,.T.);
#14716=EDGE_CURVE('',#11174,#11176,#6845,.T.);
#14717=EDGE_CURVE('',#11178,#11179,#5808,.T.);
#14718=EDGE_CURVE('',#11179,#11177,#5809,.T.);
#14719=EDGE_CURVE('',#11176,#11178,#5810,.T.);
#14720=EDGE_CURVE('',#11180,#11179,#6846,.T.);
#14721=EDGE_CURVE('',#11178,#11181,#6847,.T.);
#14722=EDGE_CURVE('',#11181,#11180,#96,.T.);
#14723=EDGE_CURVE('',#11182,#11180,#6848,.T.);
#14724=EDGE_CURVE('',#11181,#11183,#6849,.T.);
#14725=EDGE_CURVE('',#11183,#11182,#97,.T.);
#14726=EDGE_CURVE('',#11183,#11184,#6850,.T.);
#14727=EDGE_CURVE('',#11184,#11185,#5811,.T.);
#14728=EDGE_CURVE('',#11185,#11182,#6851,.T.);
#14729=EDGE_CURVE('',#11186,#11187,#5812,.T.);
#14730=EDGE_CURVE('',#11187,#11185,#5813,.T.);
#14731=EDGE_CURVE('',#11184,#11186,#5814,.T.);
#14732=EDGE_CURVE('',#11188,#11187,#6852,.T.);
#14733=EDGE_CURVE('',#11186,#11189,#6853,.T.);
#14734=EDGE_CURVE('',#11189,#11188,#98,.T.);
#14735=EDGE_CURVE('',#11160,#11188,#6854,.T.);
#14736=EDGE_CURVE('',#11189,#11161,#6855,.T.);
#14737=EDGE_CURVE('',#11159,#11190,#6856,.T.);
#14738=EDGE_CURVE('',#11190,#11191,#5815,.T.);
#14739=EDGE_CURVE('',#11191,#11156,#6857,.T.);
#14740=EDGE_CURVE('',#11192,#11193,#5816,.T.);
#14741=EDGE_CURVE('',#11193,#11191,#5817,.T.);
#14742=EDGE_CURVE('',#11190,#11192,#5818,.T.);
#14743=EDGE_CURVE('',#11194,#11193,#6858,.T.);
#14744=EDGE_CURVE('',#11192,#11195,#6859,.T.);
#14745=EDGE_CURVE('',#11195,#11194,#99,.T.);
#14746=EDGE_CURVE('',#11195,#11196,#6860,.T.);
#14747=EDGE_CURVE('',#11196,#11197,#100,.T.);
#14748=EDGE_CURVE('',#11197,#11194,#6861,.T.);
#14749=EDGE_CURVE('',#11196,#11198,#6862,.T.);
#14750=EDGE_CURVE('',#11198,#11199,#5819,.T.);
#14751=EDGE_CURVE('',#11199,#11197,#6863,.T.);
#14752=EDGE_CURVE('',#11200,#11201,#5820,.T.);
#14753=EDGE_CURVE('',#11201,#11199,#5821,.T.);
#14754=EDGE_CURVE('',#11198,#11200,#5822,.T.);
#14755=EDGE_CURVE('',#11202,#11203,#5823,.T.);
#14756=EDGE_CURVE('',#11203,#11201,#6864,.T.);
#14757=EDGE_CURVE('',#11200,#11202,#6865,.T.);
#14758=EDGE_CURVE('',#11204,#11205,#5824,.T.);
#14759=EDGE_CURVE('',#11205,#11203,#5825,.T.);
#14760=EDGE_CURVE('',#11202,#11204,#5826,.T.);
#14761=EDGE_CURVE('',#11206,#11207,#5827,.T.);
#14762=EDGE_CURVE('',#11207,#11205,#6866,.T.);
#14763=EDGE_CURVE('',#11204,#11206,#6867,.T.);
#14764=EDGE_CURVE('',#11208,#11209,#5828,.T.);
#14765=EDGE_CURVE('',#11209,#11207,#5829,.T.);
#14766=EDGE_CURVE('',#11206,#11208,#5830,.T.);
#14767=EDGE_CURVE('',#11210,#11211,#5831,.T.);
#14768=EDGE_CURVE('',#11211,#11209,#6868,.T.);
#14769=EDGE_CURVE('',#11208,#11210,#6869,.T.);
#14770=EDGE_CURVE('',#11212,#11213,#5832,.T.);
#14771=EDGE_CURVE('',#11213,#11211,#5833,.T.);
#14772=EDGE_CURVE('',#11210,#11212,#5834,.T.);
#14773=EDGE_CURVE('',#11214,#11215,#5835,.T.);
#14774=EDGE_CURVE('',#11215,#11213,#6870,.T.);
#14775=EDGE_CURVE('',#11212,#11214,#6871,.T.);
#14776=EDGE_CURVE('',#11216,#11217,#5836,.T.);
#14777=EDGE_CURVE('',#11217,#11163,#6872,.T.);
#14778=EDGE_CURVE('',#11163,#11218,#5837,.T.);
#14779=EDGE_CURVE('',#11218,#11216,#6873,.T.);
#14780=EDGE_CURVE('',#11216,#11219,#6874,.T.);
#14781=EDGE_CURVE('',#11219,#11220,#5838,.T.);
#14782=EDGE_CURVE('',#11220,#11217,#6875,.T.);
#14783=EDGE_CURVE('',#11219,#11221,#6876,.T.);
#14784=EDGE_CURVE('',#11221,#11214,#5839,.T.);
#14785=EDGE_CURVE('',#11214,#11220,#6877,.T.);
#14786=EDGE_CURVE('',#11221,#11215,#5840,.T.);
#14787=EDGE_CURVE('',#11162,#11218,#5841,.T.);
#14788=EDGE_CURVE('',#11191,#11222,#6878,.T.);
#14789=EDGE_CURVE('',#11223,#11222,#6879,.T.);
#14790=EDGE_CURVE('',#11156,#11223,#6880,.T.);
#14791=EDGE_CURVE('',#11193,#11224,#6881,.T.);
#14792=EDGE_CURVE('',#11222,#11224,#5842,.T.);
#14793=EDGE_CURVE('',#11194,#11225,#6882,.T.);
#14794=EDGE_CURVE('',#11224,#11225,#6883,.T.);
#14795=EDGE_CURVE('',#11197,#11226,#6884,.T.);
#14796=EDGE_CURVE('',#11225,#11226,#6885,.T.);
#14797=EDGE_CURVE('',#11199,#11227,#6886,.T.);
#14798=EDGE_CURVE('',#11226,#11227,#6887,.T.);
#14799=EDGE_CURVE('',#11201,#11228,#6888,.T.);
#14800=EDGE_CURVE('',#11227,#11228,#5843,.T.);
#14801=EDGE_CURVE('',#11203,#11229,#6889,.T.);
#14802=EDGE_CURVE('',#11228,#11229,#6890,.T.);
#14803=EDGE_CURVE('',#11205,#11230,#6891,.T.);
#14804=EDGE_CURVE('',#11229,#11230,#5844,.T.);
#14805=EDGE_CURVE('',#11207,#11231,#6892,.T.);
#14806=EDGE_CURVE('',#11230,#11231,#6893,.T.);
#14807=EDGE_CURVE('',#11209,#11232,#6894,.T.);
#14808=EDGE_CURVE('',#11232,#11233,#5845,.T.);
#14809=EDGE_CURVE('',#11233,#11234,#6895,.T.);
#14810=EDGE_CURVE('',#11231,#11234,#5846,.T.);
#14811=EDGE_CURVE('',#11211,#11235,#6896,.T.);
#14812=EDGE_CURVE('',#11235,#11232,#6897,.T.);
#14813=EDGE_CURVE('',#11213,#11236,#6898,.T.);
#14814=EDGE_CURVE('',#11236,#11235,#5847,.T.);
#14815=EDGE_CURVE('',#11215,#11237,#6899,.T.);
#14816=EDGE_CURVE('',#11238,#11237,#6900,.T.);
#14817=EDGE_CURVE('',#11238,#11239,#6901,.T.);
#14818=EDGE_CURVE('',#11239,#11236,#6902,.T.);
#14819=EDGE_CURVE('',#11221,#11240,#6903,.T.);
#14820=EDGE_CURVE('',#11237,#11240,#5848,.T.);
#14821=EDGE_CURVE('',#11219,#11241,#6904,.T.);
#14822=EDGE_CURVE('',#11240,#11241,#6905,.T.);
#14823=EDGE_CURVE('',#11216,#11242,#6906,.T.);
#14824=EDGE_CURVE('',#11241,#11242,#6907,.T.);
#14825=EDGE_CURVE('',#11218,#11243,#6908,.T.);
#14826=EDGE_CURVE('',#11242,#11243,#6909,.T.);
#14827=EDGE_CURVE('',#11237,#11244,#5849,.T.);
#14828=EDGE_CURVE('',#11244,#11245,#6910,.T.);
#14829=EDGE_CURVE('',#11245,#11238,#1143,.T.);
#14830=EDGE_CURVE('',#11245,#11246,#5850,.T.);
#14831=EDGE_CURVE('',#11246,#11247,#1144,.T.);
#14832=EDGE_CURVE('',#11247,#11234,#1145,.T.);
#14833=EDGE_CURVE('',#11234,#11238,#5851,.T.);
#14834=EDGE_CURVE('',#11241,#11248,#5852,.T.);
#14835=EDGE_CURVE('',#11248,#11244,#6911,.T.);
#14836=EDGE_CURVE('',#11244,#11240,#5853,.T.);
#14837=EDGE_CURVE('',#11242,#11249,#5854,.T.);
#14838=EDGE_CURVE('',#11249,#11248,#6912,.T.);
#14839=EDGE_CURVE('',#11243,#11250,#5855,.T.);
#14840=EDGE_CURVE('',#11250,#11249,#6913,.T.);
#14841=EDGE_CURVE('',#11251,#11252,#5856,.T.);
#14842=EDGE_CURVE('',#11252,#11253,#1146,.T.);
#14843=EDGE_CURVE('',#11253,#11254,#1147,.T.);
#14844=EDGE_CURVE('',#11254,#11255,#5857,.T.);
#14845=EDGE_CURVE('',#11255,#11251,#1148,.T.);
#14846=EDGE_CURVE('',#11255,#11250,#6914,.T.);
#14847=EDGE_CURVE('',#11250,#11256,#5858,.T.);
#14848=EDGE_CURVE('',#11256,#11251,#6915,.T.);
#14849=EDGE_CURVE('',#11243,#11256,#5859,.T.);
#14850=EDGE_CURVE('',#11246,#11257,#6916,.T.);
#14851=EDGE_CURVE('',#11230,#11257,#5860,.T.);
#14852=EDGE_CURVE('',#11231,#11247,#5861,.T.);
#14853=EDGE_CURVE('',#11258,#11254,#6917,.T.);
#14854=EDGE_CURVE('',#11259,#11258,#5862,.T.);
#14855=EDGE_CURVE('',#11260,#11259,#6918,.T.);
#14856=EDGE_CURVE('',#11261,#11260,#5863,.T.);
#14857=EDGE_CURVE('',#11262,#11261,#6919,.T.);
#14858=EDGE_CURVE('',#11263,#11262,#6920,.T.);
#14859=EDGE_CURVE('',#11264,#11263,#6921,.T.);
#14860=EDGE_CURVE('',#11265,#11264,#5864,.T.);
#14861=EDGE_CURVE('',#11266,#11265,#6922,.T.);
#14862=EDGE_CURVE('',#11267,#11266,#6923,.T.);
#14863=EDGE_CURVE('',#11268,#11267,#6924,.T.);
#14864=EDGE_CURVE('',#11269,#11268,#6925,.T.);
#14865=EDGE_CURVE('',#11270,#11269,#6926,.T.);
#14866=EDGE_CURVE('',#11271,#11270,#5865,.T.);
#14867=EDGE_CURVE('',#11272,#11271,#6927,.T.);
#14868=EDGE_CURVE('',#11273,#11272,#6928,.T.);
#14869=EDGE_CURVE('',#11274,#11273,#6929,.T.);
#14870=EDGE_CURVE('',#11275,#11274,#5866,.T.);
#14871=EDGE_CURVE('',#11276,#11275,#6930,.T.);
#14872=EDGE_CURVE('',#11257,#11276,#5867,.T.);
#14873=EDGE_CURVE('',#11277,#11253,#5868,.T.);
#14874=EDGE_CURVE('',#11277,#11278,#6931,.T.);
#14875=EDGE_CURVE('',#11278,#11258,#5869,.T.);
#14876=EDGE_CURVE('',#11252,#11277,#5870,.T.);
#14877=EDGE_CURVE('',#11227,#11274,#5871,.T.);
#14878=EDGE_CURVE('',#11273,#11226,#101,.T.);
#14879=EDGE_CURVE('',#11228,#11275,#5872,.T.);
#14880=EDGE_CURVE('',#11229,#11276,#5873,.T.);
#14881=EDGE_CURVE('',#11272,#11225,#102,.T.);
#14882=EDGE_CURVE('',#11222,#11270,#5874,.T.);
#14883=EDGE_CURVE('',#11269,#11223,#103,.T.);
#14884=EDGE_CURVE('',#11224,#11271,#5875,.T.);
#14885=EDGE_CURVE('',#11279,#11280,#6932,.T.);
#14886=EDGE_CURVE('',#11280,#11267,#5876,.T.);
#14887=EDGE_CURVE('',#11266,#11279,#104,.T.);
#14888=EDGE_CURVE('',#11281,#11268,#5877,.T.);
#14889=EDGE_CURVE('',#11280,#11281,#6933,.T.);
#14890=EDGE_CURVE('',#11281,#11223,#6934,.T.);
#14891=EDGE_CURVE('',#11282,#11283,#6935,.T.);
#14892=EDGE_CURVE('',#11283,#11264,#5878,.T.);
#14893=EDGE_CURVE('',#11263,#11282,#105,.T.);
#14894=EDGE_CURVE('',#11284,#11265,#5879,.T.);
#14895=EDGE_CURVE('',#11283,#11284,#5880,.T.);
#14896=EDGE_CURVE('',#11284,#11279,#6936,.T.);
#14897=EDGE_CURVE('',#11285,#11282,#6937,.T.);
#14898=EDGE_CURVE('',#11262,#11285,#106,.T.);
#14899=EDGE_CURVE('',#11286,#11259,#5881,.T.);
#14900=EDGE_CURVE('',#11278,#11286,#5882,.T.);
#14901=EDGE_CURVE('',#11287,#11260,#5883,.T.);
#14902=EDGE_CURVE('',#11286,#11287,#6938,.T.);
#14903=EDGE_CURVE('',#11288,#11261,#5884,.T.);
#14904=EDGE_CURVE('',#11287,#11288,#5885,.T.);
#14905=EDGE_CURVE('',#11288,#11285,#6939,.T.);
#14906=EDGE_CURVE('',#11157,#11281,#6940,.T.);
#14907=EDGE_CURVE('',#11160,#11280,#6941,.T.);
#14908=EDGE_CURVE('',#11188,#11279,#6942,.T.);
#14909=EDGE_CURVE('',#11187,#11284,#6943,.T.);
#14910=EDGE_CURVE('',#11185,#11283,#6944,.T.);
#14911=EDGE_CURVE('',#11182,#11282,#6945,.T.);
#14912=EDGE_CURVE('',#11180,#11285,#6946,.T.);
#14913=EDGE_CURVE('',#11179,#11288,#6947,.T.);
#14914=EDGE_CURVE('',#11177,#11287,#6948,.T.);
#14915=EDGE_CURVE('',#11175,#11286,#6949,.T.);
#14916=EDGE_CURVE('',#11173,#11278,#6950,.T.);
#14917=EDGE_CURVE('',#11171,#11277,#6951,.T.);
#14918=EDGE_CURVE('',#11252,#11289,#6952,.T.);
#14919=EDGE_CURVE('',#11289,#11290,#5886,.T.);
#14920=EDGE_CURVE('',#11169,#11290,#6953,.T.);
#14921=EDGE_CURVE('',#11291,#11251,#6954,.T.);
#14922=EDGE_CURVE('',#11291,#11289,#5887,.T.);
#14923=EDGE_CURVE('',#11233,#11239,#5888,.T.);
#14924=EDGE_CURVE('',#11290,#11292,#6955,.T.);
#14925=EDGE_CURVE('',#11293,#11291,#6956,.T.);
#14926=EDGE_CURVE('',#11292,#11293,#5889,.T.);
#14927=EDGE_CURVE('',#11167,#11292,#6957,.T.);
#14928=EDGE_CURVE('',#11165,#11293,#6958,.T.);
#14929=EDGE_CURVE('',#11162,#11256,#6959,.T.);
#20641=ORIENTED_EDGE('',*,*,#14682,.F.);
#20642=ORIENTED_EDGE('',*,*,#14683,.T.);
#20643=ORIENTED_EDGE('',*,*,#14684,.F.);
#20644=ORIENTED_EDGE('',*,*,#14683,.F.);
#20645=ORIENTED_EDGE('',*,*,#14682,.T.);
#20646=ORIENTED_EDGE('',*,*,#14685,.F.);
#20647=ORIENTED_EDGE('',*,*,#14686,.T.);
#20648=ORIENTED_EDGE('',*,*,#14687,.T.);
#20649=ORIENTED_EDGE('',*,*,#14686,.F.);
#20650=ORIENTED_EDGE('',*,*,#14687,.F.);
#20651=ORIENTED_EDGE('',*,*,#14688,.T.);
#20652=ORIENTED_EDGE('',*,*,#14689,.T.);
#20653=ORIENTED_EDGE('',*,*,#14690,.T.);
#20654=ORIENTED_EDGE('',*,*,#14691,.T.);
#20655=ORIENTED_EDGE('',*,*,#14689,.F.);
#20656=ORIENTED_EDGE('',*,*,#14692,.T.);
#20657=ORIENTED_EDGE('',*,*,#14693,.T.);
#20658=ORIENTED_EDGE('',*,*,#14694,.T.);
#20659=ORIENTED_EDGE('',*,*,#14695,.T.);
#20660=ORIENTED_EDGE('',*,*,#14696,.T.);
#20661=ORIENTED_EDGE('',*,*,#14697,.T.);
#20662=ORIENTED_EDGE('',*,*,#14698,.T.);
#20663=ORIENTED_EDGE('',*,*,#14699,.T.);
#20664=ORIENTED_EDGE('',*,*,#14700,.T.);
#20665=ORIENTED_EDGE('',*,*,#14697,.F.);
#20666=ORIENTED_EDGE('',*,*,#14701,.T.);
#20667=ORIENTED_EDGE('',*,*,#14702,.T.);
#20668=ORIENTED_EDGE('',*,*,#14703,.T.);
#20669=ORIENTED_EDGE('',*,*,#14699,.F.);
#20670=ORIENTED_EDGE('',*,*,#14704,.T.);
#20671=ORIENTED_EDGE('',*,*,#14705,.T.);
#20672=ORIENTED_EDGE('',*,*,#14706,.T.);
#20673=ORIENTED_EDGE('',*,*,#14702,.F.);
#20674=ORIENTED_EDGE('',*,*,#14707,.T.);
#20675=ORIENTED_EDGE('',*,*,#14708,.T.);
#20676=ORIENTED_EDGE('',*,*,#14709,.T.);
#20677=ORIENTED_EDGE('',*,*,#14705,.F.);
#20678=ORIENTED_EDGE('',*,*,#14710,.T.);
#20679=ORIENTED_EDGE('',*,*,#14711,.T.);
#20680=ORIENTED_EDGE('',*,*,#14712,.T.);
#20681=ORIENTED_EDGE('',*,*,#14708,.F.);
#20682=ORIENTED_EDGE('',*,*,#14713,.T.);
#20683=ORIENTED_EDGE('',*,*,#14714,.T.);
#20684=ORIENTED_EDGE('',*,*,#14715,.T.);
#20685=ORIENTED_EDGE('',*,*,#14711,.F.);
#20686=ORIENTED_EDGE('',*,*,#14716,.T.);
#20687=ORIENTED_EDGE('',*,*,#14717,.T.);
#20688=ORIENTED_EDGE('',*,*,#14718,.T.);
#20689=ORIENTED_EDGE('',*,*,#14714,.F.);
#20690=ORIENTED_EDGE('',*,*,#14719,.T.);
#20691=ORIENTED_EDGE('',*,*,#14720,.T.);
#20692=ORIENTED_EDGE('',*,*,#14717,.F.);
#20693=ORIENTED_EDGE('',*,*,#14721,.T.);
#20694=ORIENTED_EDGE('',*,*,#14722,.T.);
#20695=ORIENTED_EDGE('',*,*,#14723,.T.);
#20696=ORIENTED_EDGE('',*,*,#14722,.F.);
#20697=ORIENTED_EDGE('',*,*,#14724,.T.);
#20698=ORIENTED_EDGE('',*,*,#14725,.T.);
#20699=ORIENTED_EDGE('',*,*,#14726,.T.);
#20700=ORIENTED_EDGE('',*,*,#14727,.T.);
#20701=ORIENTED_EDGE('',*,*,#14728,.T.);
#20702=ORIENTED_EDGE('',*,*,#14725,.F.);
#20703=ORIENTED_EDGE('',*,*,#14729,.T.);
#20704=ORIENTED_EDGE('',*,*,#14730,.T.);
#20705=ORIENTED_EDGE('',*,*,#14727,.F.);
#20706=ORIENTED_EDGE('',*,*,#14731,.T.);
#20707=ORIENTED_EDGE('',*,*,#14732,.T.);
#20708=ORIENTED_EDGE('',*,*,#14729,.F.);
#20709=ORIENTED_EDGE('',*,*,#14733,.T.);
#20710=ORIENTED_EDGE('',*,*,#14734,.T.);
#20711=ORIENTED_EDGE('',*,*,#14693,.F.);
#20712=ORIENTED_EDGE('',*,*,#14735,.T.);
#20713=ORIENTED_EDGE('',*,*,#14734,.F.);
#20714=ORIENTED_EDGE('',*,*,#14736,.T.);
#20715=ORIENTED_EDGE('',*,*,#14737,.T.);
#20716=ORIENTED_EDGE('',*,*,#14738,.T.);
#20717=ORIENTED_EDGE('',*,*,#14739,.T.);
#20718=ORIENTED_EDGE('',*,*,#14691,.F.);
#20719=ORIENTED_EDGE('',*,*,#14740,.T.);
#20720=ORIENTED_EDGE('',*,*,#14741,.T.);
#20721=ORIENTED_EDGE('',*,*,#14738,.F.);
#20722=ORIENTED_EDGE('',*,*,#14742,.T.);
#20723=ORIENTED_EDGE('',*,*,#14743,.T.);
#20724=ORIENTED_EDGE('',*,*,#14740,.F.);
#20725=ORIENTED_EDGE('',*,*,#14744,.T.);
#20726=ORIENTED_EDGE('',*,*,#14745,.T.);
#20727=ORIENTED_EDGE('',*,*,#14746,.T.);
#20728=ORIENTED_EDGE('',*,*,#14747,.T.);
#20729=ORIENTED_EDGE('',*,*,#14748,.T.);
#20730=ORIENTED_EDGE('',*,*,#14745,.F.);
#20731=ORIENTED_EDGE('',*,*,#14749,.T.);
#20732=ORIENTED_EDGE('',*,*,#14750,.T.);
#20733=ORIENTED_EDGE('',*,*,#14751,.T.);
#20734=ORIENTED_EDGE('',*,*,#14747,.F.);
#20735=ORIENTED_EDGE('',*,*,#14752,.T.);
#20736=ORIENTED_EDGE('',*,*,#14753,.T.);
#20737=ORIENTED_EDGE('',*,*,#14750,.F.);
#20738=ORIENTED_EDGE('',*,*,#14754,.T.);
#20739=ORIENTED_EDGE('',*,*,#14755,.T.);
#20740=ORIENTED_EDGE('',*,*,#14756,.T.);
#20741=ORIENTED_EDGE('',*,*,#14752,.F.);
#20742=ORIENTED_EDGE('',*,*,#14757,.T.);
#20743=ORIENTED_EDGE('',*,*,#14758,.T.);
#20744=ORIENTED_EDGE('',*,*,#14759,.T.);
#20745=ORIENTED_EDGE('',*,*,#14755,.F.);
#20746=ORIENTED_EDGE('',*,*,#14760,.T.);
#20747=ORIENTED_EDGE('',*,*,#14761,.T.);
#20748=ORIENTED_EDGE('',*,*,#14762,.T.);
#20749=ORIENTED_EDGE('',*,*,#14758,.F.);
#20750=ORIENTED_EDGE('',*,*,#14763,.T.);
#20751=ORIENTED_EDGE('',*,*,#14764,.T.);
#20752=ORIENTED_EDGE('',*,*,#14765,.T.);
#20753=ORIENTED_EDGE('',*,*,#14761,.F.);
#20754=ORIENTED_EDGE('',*,*,#14766,.T.);
#20755=ORIENTED_EDGE('',*,*,#14767,.T.);
#20756=ORIENTED_EDGE('',*,*,#14768,.T.);
#20757=ORIENTED_EDGE('',*,*,#14764,.F.);
#20758=ORIENTED_EDGE('',*,*,#14769,.T.);
#20759=ORIENTED_EDGE('',*,*,#14770,.T.);
#20760=ORIENTED_EDGE('',*,*,#14771,.T.);
#20761=ORIENTED_EDGE('',*,*,#14767,.F.);
#20762=ORIENTED_EDGE('',*,*,#14772,.T.);
#20763=ORIENTED_EDGE('',*,*,#14773,.T.);
#20764=ORIENTED_EDGE('',*,*,#14774,.T.);
#20765=ORIENTED_EDGE('',*,*,#14770,.F.);
#20766=ORIENTED_EDGE('',*,*,#14775,.T.);
#20767=ORIENTED_EDGE('',*,*,#14776,.T.);
#20768=ORIENTED_EDGE('',*,*,#14777,.T.);
#20769=ORIENTED_EDGE('',*,*,#14778,.T.);
#20770=ORIENTED_EDGE('',*,*,#14779,.T.);
#20771=ORIENTED_EDGE('',*,*,#14776,.F.);
#20772=ORIENTED_EDGE('',*,*,#14780,.T.);
#20773=ORIENTED_EDGE('',*,*,#14781,.T.);
#20774=ORIENTED_EDGE('',*,*,#14782,.T.);
#20775=ORIENTED_EDGE('',*,*,#14781,.F.);
#20776=ORIENTED_EDGE('',*,*,#14783,.T.);
#20777=ORIENTED_EDGE('',*,*,#14784,.T.);
#20778=ORIENTED_EDGE('',*,*,#14785,.T.);
#20779=ORIENTED_EDGE('',*,*,#14784,.F.);
#20780=ORIENTED_EDGE('',*,*,#14786,.T.);
#20781=ORIENTED_EDGE('',*,*,#14773,.F.);
#20782=ORIENTED_EDGE('',*,*,#14695,.F.);
#20783=ORIENTED_EDGE('',*,*,#14787,.T.);
#20784=ORIENTED_EDGE('',*,*,#14778,.F.);
#20785=ORIENTED_EDGE('',*,*,#14739,.F.);
#20786=ORIENTED_EDGE('',*,*,#14788,.T.);
#20787=ORIENTED_EDGE('',*,*,#14789,.F.);
#20788=ORIENTED_EDGE('',*,*,#14790,.F.);
#20789=ORIENTED_EDGE('',*,*,#14741,.F.);
#20790=ORIENTED_EDGE('',*,*,#14791,.T.);
#20791=ORIENTED_EDGE('',*,*,#14792,.F.);
#20792=ORIENTED_EDGE('',*,*,#14788,.F.);
#20793=ORIENTED_EDGE('',*,*,#14743,.F.);
#20794=ORIENTED_EDGE('',*,*,#14793,.T.);
#20795=ORIENTED_EDGE('',*,*,#14794,.F.);
#20796=ORIENTED_EDGE('',*,*,#14791,.F.);
#20797=ORIENTED_EDGE('',*,*,#14748,.F.);
#20798=ORIENTED_EDGE('',*,*,#14795,.T.);
#20799=ORIENTED_EDGE('',*,*,#14796,.F.);
#20800=ORIENTED_EDGE('',*,*,#14793,.F.);
#20801=ORIENTED_EDGE('',*,*,#14751,.F.);
#20802=ORIENTED_EDGE('',*,*,#14797,.T.);
#20803=ORIENTED_EDGE('',*,*,#14798,.F.);
#20804=ORIENTED_EDGE('',*,*,#14795,.F.);
#20805=ORIENTED_EDGE('',*,*,#14753,.F.);
#20806=ORIENTED_EDGE('',*,*,#14799,.T.);
#20807=ORIENTED_EDGE('',*,*,#14800,.F.);
#20808=ORIENTED_EDGE('',*,*,#14797,.F.);
#20809=ORIENTED_EDGE('',*,*,#14756,.F.);
#20810=ORIENTED_EDGE('',*,*,#14801,.T.);
#20811=ORIENTED_EDGE('',*,*,#14802,.F.);
#20812=ORIENTED_EDGE('',*,*,#14799,.F.);
#20813=ORIENTED_EDGE('',*,*,#14685,.T.);
#20814=ORIENTED_EDGE('',*,*,#14759,.F.);
#20815=ORIENTED_EDGE('',*,*,#14803,.T.);
#20816=ORIENTED_EDGE('',*,*,#14804,.F.);
#20817=ORIENTED_EDGE('',*,*,#14801,.F.);
#20818=ORIENTED_EDGE('',*,*,#14762,.F.);
#20819=ORIENTED_EDGE('',*,*,#14805,.T.);
#20820=ORIENTED_EDGE('',*,*,#14806,.F.);
#20821=ORIENTED_EDGE('',*,*,#14803,.F.);
#20822=ORIENTED_EDGE('',*,*,#14765,.F.);
#20823=ORIENTED_EDGE('',*,*,#14807,.T.);
#20824=ORIENTED_EDGE('',*,*,#14808,.T.);
#20825=ORIENTED_EDGE('',*,*,#14809,.T.);
#20826=ORIENTED_EDGE('',*,*,#14810,.F.);
#20827=ORIENTED_EDGE('',*,*,#14805,.F.);
#20828=ORIENTED_EDGE('',*,*,#14768,.F.);
#20829=ORIENTED_EDGE('',*,*,#14811,.T.);
#20830=ORIENTED_EDGE('',*,*,#14812,.T.);
#20831=ORIENTED_EDGE('',*,*,#14807,.F.);
#20832=ORIENTED_EDGE('',*,*,#14771,.F.);
#20833=ORIENTED_EDGE('',*,*,#14813,.T.);
#20834=ORIENTED_EDGE('',*,*,#14814,.T.);
#20835=ORIENTED_EDGE('',*,*,#14811,.F.);
#20836=ORIENTED_EDGE('',*,*,#14774,.F.);
#20837=ORIENTED_EDGE('',*,*,#14815,.T.);
#20838=ORIENTED_EDGE('',*,*,#14816,.F.);
#20839=ORIENTED_EDGE('',*,*,#14817,.T.);
#20840=ORIENTED_EDGE('',*,*,#14818,.T.);
#20841=ORIENTED_EDGE('',*,*,#14813,.F.);
#20842=ORIENTED_EDGE('',*,*,#14786,.F.);
#20843=ORIENTED_EDGE('',*,*,#14819,.T.);
#20844=ORIENTED_EDGE('',*,*,#14820,.F.);
#20845=ORIENTED_EDGE('',*,*,#14815,.F.);
#20846=ORIENTED_EDGE('',*,*,#14783,.F.);
#20847=ORIENTED_EDGE('',*,*,#14821,.T.);
#20848=ORIENTED_EDGE('',*,*,#14822,.F.);
#20849=ORIENTED_EDGE('',*,*,#14819,.F.);
#20850=ORIENTED_EDGE('',*,*,#14780,.F.);
#20851=ORIENTED_EDGE('',*,*,#14823,.T.);
#20852=ORIENTED_EDGE('',*,*,#14824,.F.);
#20853=ORIENTED_EDGE('',*,*,#14821,.F.);
#20854=ORIENTED_EDGE('',*,*,#14779,.F.);
#20855=ORIENTED_EDGE('',*,*,#14825,.T.);
#20856=ORIENTED_EDGE('',*,*,#14826,.F.);
#20857=ORIENTED_EDGE('',*,*,#14823,.F.);
#20858=ORIENTED_EDGE('',*,*,#14696,.F.);
#20859=ORIENTED_EDGE('',*,*,#14777,.F.);
#20860=ORIENTED_EDGE('',*,*,#14782,.F.);
#20861=ORIENTED_EDGE('',*,*,#14785,.F.);
#20862=ORIENTED_EDGE('',*,*,#14775,.F.);
#20863=ORIENTED_EDGE('',*,*,#14772,.F.);
#20864=ORIENTED_EDGE('',*,*,#14769,.F.);
#20865=ORIENTED_EDGE('',*,*,#14766,.F.);
#20866=ORIENTED_EDGE('',*,*,#14763,.F.);
#20867=ORIENTED_EDGE('',*,*,#14760,.F.);
#20868=ORIENTED_EDGE('',*,*,#14757,.F.);
#20869=ORIENTED_EDGE('',*,*,#14754,.F.);
#20870=ORIENTED_EDGE('',*,*,#14749,.F.);
#20871=ORIENTED_EDGE('',*,*,#14746,.F.);
#20872=ORIENTED_EDGE('',*,*,#14744,.F.);
#20873=ORIENTED_EDGE('',*,*,#14742,.F.);
#20874=ORIENTED_EDGE('',*,*,#14737,.F.);
#20875=ORIENTED_EDGE('',*,*,#14690,.F.);
#20876=ORIENTED_EDGE('',*,*,#14694,.F.);
#20877=ORIENTED_EDGE('',*,*,#14736,.F.);
#20878=ORIENTED_EDGE('',*,*,#14733,.F.);
#20879=ORIENTED_EDGE('',*,*,#14731,.F.);
#20880=ORIENTED_EDGE('',*,*,#14726,.F.);
#20881=ORIENTED_EDGE('',*,*,#14724,.F.);
#20882=ORIENTED_EDGE('',*,*,#14721,.F.);
#20883=ORIENTED_EDGE('',*,*,#14719,.F.);
#20884=ORIENTED_EDGE('',*,*,#14716,.F.);
#20885=ORIENTED_EDGE('',*,*,#14713,.F.);
#20886=ORIENTED_EDGE('',*,*,#14710,.F.);
#20887=ORIENTED_EDGE('',*,*,#14707,.F.);
#20888=ORIENTED_EDGE('',*,*,#14704,.F.);
#20889=ORIENTED_EDGE('',*,*,#14701,.F.);
#20890=ORIENTED_EDGE('',*,*,#14816,.T.);
#20891=ORIENTED_EDGE('',*,*,#14827,.T.);
#20892=ORIENTED_EDGE('',*,*,#14828,.T.);
#20893=ORIENTED_EDGE('',*,*,#14829,.T.);
#20894=ORIENTED_EDGE('',*,*,#14830,.T.);
#20895=ORIENTED_EDGE('',*,*,#14831,.T.);
#20896=ORIENTED_EDGE('',*,*,#14832,.T.);
#20897=ORIENTED_EDGE('',*,*,#14833,.T.);
#20898=ORIENTED_EDGE('',*,*,#14829,.F.);
#20899=ORIENTED_EDGE('',*,*,#14834,.T.);
#20900=ORIENTED_EDGE('',*,*,#14835,.T.);
#20901=ORIENTED_EDGE('',*,*,#14836,.T.);
#20902=ORIENTED_EDGE('',*,*,#14822,.T.);
#20903=ORIENTED_EDGE('',*,*,#14837,.T.);
#20904=ORIENTED_EDGE('',*,*,#14838,.T.);
#20905=ORIENTED_EDGE('',*,*,#14834,.F.);
#20906=ORIENTED_EDGE('',*,*,#14824,.T.);
#20907=ORIENTED_EDGE('',*,*,#14837,.F.);
#20908=ORIENTED_EDGE('',*,*,#14826,.T.);
#20909=ORIENTED_EDGE('',*,*,#14839,.T.);
#20910=ORIENTED_EDGE('',*,*,#14840,.T.);
#20911=ORIENTED_EDGE('',*,*,#14836,.F.);
#20912=ORIENTED_EDGE('',*,*,#14827,.F.);
#20913=ORIENTED_EDGE('',*,*,#14820,.T.);
#20914=ORIENTED_EDGE('',*,*,#14841,.T.);
#20915=ORIENTED_EDGE('',*,*,#14842,.T.);
#20916=ORIENTED_EDGE('',*,*,#14843,.T.);
#20917=ORIENTED_EDGE('',*,*,#14844,.T.);
#20918=ORIENTED_EDGE('',*,*,#14845,.T.);
#20919=ORIENTED_EDGE('',*,*,#14846,.T.);
#20920=ORIENTED_EDGE('',*,*,#14847,.T.);
#20921=ORIENTED_EDGE('',*,*,#14848,.T.);
#20922=ORIENTED_EDGE('',*,*,#14845,.F.);
#20923=ORIENTED_EDGE('',*,*,#14847,.F.);
#20924=ORIENTED_EDGE('',*,*,#14839,.F.);
#20925=ORIENTED_EDGE('',*,*,#14849,.T.);
#20926=ORIENTED_EDGE('',*,*,#14831,.F.);
#20927=ORIENTED_EDGE('',*,*,#14850,.T.);
#20928=ORIENTED_EDGE('',*,*,#14851,.F.);
#20929=ORIENTED_EDGE('',*,*,#14806,.T.);
#20930=ORIENTED_EDGE('',*,*,#14852,.T.);
#20931=ORIENTED_EDGE('',*,*,#14830,.F.);
#20932=ORIENTED_EDGE('',*,*,#14828,.F.);
#20933=ORIENTED_EDGE('',*,*,#14835,.F.);
#20934=ORIENTED_EDGE('',*,*,#14838,.F.);
#20935=ORIENTED_EDGE('',*,*,#14840,.F.);
#20936=ORIENTED_EDGE('',*,*,#14846,.F.);
#20937=ORIENTED_EDGE('',*,*,#14844,.F.);
#20938=ORIENTED_EDGE('',*,*,#14853,.F.);
#20939=ORIENTED_EDGE('',*,*,#14854,.F.);
#20940=ORIENTED_EDGE('',*,*,#14855,.F.);
#20941=ORIENTED_EDGE('',*,*,#14856,.F.);
#20942=ORIENTED_EDGE('',*,*,#14857,.F.);
#20943=ORIENTED_EDGE('',*,*,#14858,.F.);
#20944=ORIENTED_EDGE('',*,*,#14859,.F.);
#20945=ORIENTED_EDGE('',*,*,#14860,.F.);
#20946=ORIENTED_EDGE('',*,*,#14861,.F.);
#20947=ORIENTED_EDGE('',*,*,#14862,.F.);
#20948=ORIENTED_EDGE('',*,*,#14863,.F.);
#20949=ORIENTED_EDGE('',*,*,#14864,.F.);
#20950=ORIENTED_EDGE('',*,*,#14865,.F.);
#20951=ORIENTED_EDGE('',*,*,#14866,.F.);
#20952=ORIENTED_EDGE('',*,*,#14867,.F.);
#20953=ORIENTED_EDGE('',*,*,#14868,.F.);
#20954=ORIENTED_EDGE('',*,*,#14869,.F.);
#20955=ORIENTED_EDGE('',*,*,#14870,.F.);
#20956=ORIENTED_EDGE('',*,*,#14871,.F.);
#20957=ORIENTED_EDGE('',*,*,#14872,.F.);
#20958=ORIENTED_EDGE('',*,*,#14850,.F.);
#20959=ORIENTED_EDGE('',*,*,#14843,.F.);
#20960=ORIENTED_EDGE('',*,*,#14873,.F.);
#20961=ORIENTED_EDGE('',*,*,#14874,.T.);
#20962=ORIENTED_EDGE('',*,*,#14875,.T.);
#20963=ORIENTED_EDGE('',*,*,#14853,.T.);
#20964=ORIENTED_EDGE('',*,*,#14842,.F.);
#20965=ORIENTED_EDGE('',*,*,#14876,.T.);
#20966=ORIENTED_EDGE('',*,*,#14873,.T.);
#20967=ORIENTED_EDGE('',*,*,#14798,.T.);
#20968=ORIENTED_EDGE('',*,*,#14877,.T.);
#20969=ORIENTED_EDGE('',*,*,#14869,.T.);
#20970=ORIENTED_EDGE('',*,*,#14878,.T.);
#20971=ORIENTED_EDGE('',*,*,#14879,.T.);
#20972=ORIENTED_EDGE('',*,*,#14870,.T.);
#20973=ORIENTED_EDGE('',*,*,#14877,.F.);
#20974=ORIENTED_EDGE('',*,*,#14800,.T.);
#20975=ORIENTED_EDGE('',*,*,#14880,.T.);
#20976=ORIENTED_EDGE('',*,*,#14871,.T.);
#20977=ORIENTED_EDGE('',*,*,#14879,.F.);
#20978=ORIENTED_EDGE('',*,*,#14802,.T.);
#20979=ORIENTED_EDGE('',*,*,#14851,.T.);
#20980=ORIENTED_EDGE('',*,*,#14872,.T.);
#20981=ORIENTED_EDGE('',*,*,#14880,.F.);
#20982=ORIENTED_EDGE('',*,*,#14804,.T.);
#20983=ORIENTED_EDGE('',*,*,#14832,.F.);
#20984=ORIENTED_EDGE('',*,*,#14852,.F.);
#20985=ORIENTED_EDGE('',*,*,#14810,.T.);
#20986=ORIENTED_EDGE('',*,*,#14796,.T.);
#20987=ORIENTED_EDGE('',*,*,#14878,.F.);
#20988=ORIENTED_EDGE('',*,*,#14868,.T.);
#20989=ORIENTED_EDGE('',*,*,#14881,.T.);
#20990=ORIENTED_EDGE('',*,*,#14789,.T.);
#20991=ORIENTED_EDGE('',*,*,#14882,.T.);
#20992=ORIENTED_EDGE('',*,*,#14865,.T.);
#20993=ORIENTED_EDGE('',*,*,#14883,.T.);
#20994=ORIENTED_EDGE('',*,*,#14884,.T.);
#20995=ORIENTED_EDGE('',*,*,#14866,.T.);
#20996=ORIENTED_EDGE('',*,*,#14882,.F.);
#20997=ORIENTED_EDGE('',*,*,#14792,.T.);
#20998=ORIENTED_EDGE('',*,*,#14867,.T.);
#20999=ORIENTED_EDGE('',*,*,#14884,.F.);
#21000=ORIENTED_EDGE('',*,*,#14794,.T.);
#21001=ORIENTED_EDGE('',*,*,#14881,.F.);
#21002=ORIENTED_EDGE('',*,*,#14885,.T.);
#21003=ORIENTED_EDGE('',*,*,#14886,.T.);
#21004=ORIENTED_EDGE('',*,*,#14862,.T.);
#21005=ORIENTED_EDGE('',*,*,#14887,.T.);
#21006=ORIENTED_EDGE('',*,*,#14888,.T.);
#21007=ORIENTED_EDGE('',*,*,#14863,.T.);
#21008=ORIENTED_EDGE('',*,*,#14886,.F.);
#21009=ORIENTED_EDGE('',*,*,#14889,.T.);
#21010=ORIENTED_EDGE('',*,*,#14864,.T.);
#21011=ORIENTED_EDGE('',*,*,#14888,.F.);
#21012=ORIENTED_EDGE('',*,*,#14890,.T.);
#21013=ORIENTED_EDGE('',*,*,#14883,.F.);
#21014=ORIENTED_EDGE('',*,*,#14891,.T.);
#21015=ORIENTED_EDGE('',*,*,#14892,.T.);
#21016=ORIENTED_EDGE('',*,*,#14859,.T.);
#21017=ORIENTED_EDGE('',*,*,#14893,.T.);
#21018=ORIENTED_EDGE('',*,*,#14894,.T.);
#21019=ORIENTED_EDGE('',*,*,#14860,.T.);
#21020=ORIENTED_EDGE('',*,*,#14892,.F.);
#21021=ORIENTED_EDGE('',*,*,#14895,.T.);
#21022=ORIENTED_EDGE('',*,*,#14861,.T.);
#21023=ORIENTED_EDGE('',*,*,#14894,.F.);
#21024=ORIENTED_EDGE('',*,*,#14896,.T.);
#21025=ORIENTED_EDGE('',*,*,#14887,.F.);
#21026=ORIENTED_EDGE('',*,*,#14897,.T.);
#21027=ORIENTED_EDGE('',*,*,#14893,.F.);
#21028=ORIENTED_EDGE('',*,*,#14858,.T.);
#21029=ORIENTED_EDGE('',*,*,#14898,.T.);
#21030=ORIENTED_EDGE('',*,*,#14899,.T.);
#21031=ORIENTED_EDGE('',*,*,#14854,.T.);
#21032=ORIENTED_EDGE('',*,*,#14875,.F.);
#21033=ORIENTED_EDGE('',*,*,#14900,.T.);
#21034=ORIENTED_EDGE('',*,*,#14901,.T.);
#21035=ORIENTED_EDGE('',*,*,#14855,.T.);
#21036=ORIENTED_EDGE('',*,*,#14899,.F.);
#21037=ORIENTED_EDGE('',*,*,#14902,.T.);
#21038=ORIENTED_EDGE('',*,*,#14903,.T.);
#21039=ORIENTED_EDGE('',*,*,#14856,.T.);
#21040=ORIENTED_EDGE('',*,*,#14901,.F.);
#21041=ORIENTED_EDGE('',*,*,#14904,.T.);
#21042=ORIENTED_EDGE('',*,*,#14857,.T.);
#21043=ORIENTED_EDGE('',*,*,#14903,.F.);
#21044=ORIENTED_EDGE('',*,*,#14905,.T.);
#21045=ORIENTED_EDGE('',*,*,#14898,.F.);
#21046=ORIENTED_EDGE('',*,*,#14688,.F.);
#21047=ORIENTED_EDGE('',*,*,#14790,.T.);
#21048=ORIENTED_EDGE('',*,*,#14890,.F.);
#21049=ORIENTED_EDGE('',*,*,#14906,.F.);
#21050=ORIENTED_EDGE('',*,*,#14692,.F.);
#21051=ORIENTED_EDGE('',*,*,#14906,.T.);
#21052=ORIENTED_EDGE('',*,*,#14889,.F.);
#21053=ORIENTED_EDGE('',*,*,#14907,.F.);
#21054=ORIENTED_EDGE('',*,*,#14735,.F.);
#21055=ORIENTED_EDGE('',*,*,#14907,.T.);
#21056=ORIENTED_EDGE('',*,*,#14885,.F.);
#21057=ORIENTED_EDGE('',*,*,#14908,.F.);
#21058=ORIENTED_EDGE('',*,*,#14732,.F.);
#21059=ORIENTED_EDGE('',*,*,#14908,.T.);
#21060=ORIENTED_EDGE('',*,*,#14896,.F.);
#21061=ORIENTED_EDGE('',*,*,#14909,.F.);
#21062=ORIENTED_EDGE('',*,*,#14730,.F.);
#21063=ORIENTED_EDGE('',*,*,#14909,.T.);
#21064=ORIENTED_EDGE('',*,*,#14895,.F.);
#21065=ORIENTED_EDGE('',*,*,#14910,.F.);
#21066=ORIENTED_EDGE('',*,*,#14728,.F.);
#21067=ORIENTED_EDGE('',*,*,#14910,.T.);
#21068=ORIENTED_EDGE('',*,*,#14891,.F.);
#21069=ORIENTED_EDGE('',*,*,#14911,.F.);
#21070=ORIENTED_EDGE('',*,*,#14723,.F.);
#21071=ORIENTED_EDGE('',*,*,#14911,.T.);
#21072=ORIENTED_EDGE('',*,*,#14897,.F.);
#21073=ORIENTED_EDGE('',*,*,#14912,.F.);
#21074=ORIENTED_EDGE('',*,*,#14720,.F.);
#21075=ORIENTED_EDGE('',*,*,#14912,.T.);
#21076=ORIENTED_EDGE('',*,*,#14905,.F.);
#21077=ORIENTED_EDGE('',*,*,#14913,.F.);
#21078=ORIENTED_EDGE('',*,*,#14718,.F.);
#21079=ORIENTED_EDGE('',*,*,#14913,.T.);
#21080=ORIENTED_EDGE('',*,*,#14904,.F.);
#21081=ORIENTED_EDGE('',*,*,#14914,.F.);
#21082=ORIENTED_EDGE('',*,*,#14715,.F.);
#21083=ORIENTED_EDGE('',*,*,#14914,.T.);
#21084=ORIENTED_EDGE('',*,*,#14902,.F.);
#21085=ORIENTED_EDGE('',*,*,#14915,.F.);
#21086=ORIENTED_EDGE('',*,*,#14684,.T.);
#21087=ORIENTED_EDGE('',*,*,#14712,.F.);
#21088=ORIENTED_EDGE('',*,*,#14915,.T.);
#21089=ORIENTED_EDGE('',*,*,#14900,.F.);
#21090=ORIENTED_EDGE('',*,*,#14916,.F.);
#21091=ORIENTED_EDGE('',*,*,#14709,.F.);
#21092=ORIENTED_EDGE('',*,*,#14916,.T.);
#21093=ORIENTED_EDGE('',*,*,#14874,.F.);
#21094=ORIENTED_EDGE('',*,*,#14917,.F.);
#21095=ORIENTED_EDGE('',*,*,#14706,.F.);
#21096=ORIENTED_EDGE('',*,*,#14917,.T.);
#21097=ORIENTED_EDGE('',*,*,#14876,.F.);
#21098=ORIENTED_EDGE('',*,*,#14918,.T.);
#21099=ORIENTED_EDGE('',*,*,#14919,.T.);
#21100=ORIENTED_EDGE('',*,*,#14920,.F.);
#21101=ORIENTED_EDGE('',*,*,#14841,.F.);
#21102=ORIENTED_EDGE('',*,*,#14921,.F.);
#21103=ORIENTED_EDGE('',*,*,#14922,.T.);
#21104=ORIENTED_EDGE('',*,*,#14918,.F.);
#21105=ORIENTED_EDGE('',*,*,#14833,.F.);
#21106=ORIENTED_EDGE('',*,*,#14809,.F.);
#21107=ORIENTED_EDGE('',*,*,#14923,.T.);
#21108=ORIENTED_EDGE('',*,*,#14817,.F.);
#21109=ORIENTED_EDGE('',*,*,#14818,.F.);
#21110=ORIENTED_EDGE('',*,*,#14923,.F.);
#21111=ORIENTED_EDGE('',*,*,#14808,.F.);
#21112=ORIENTED_EDGE('',*,*,#14812,.F.);
#21113=ORIENTED_EDGE('',*,*,#14814,.F.);
#21114=ORIENTED_EDGE('',*,*,#14924,.F.);
#21115=ORIENTED_EDGE('',*,*,#14919,.F.);
#21116=ORIENTED_EDGE('',*,*,#14922,.F.);
#21117=ORIENTED_EDGE('',*,*,#14925,.F.);
#21118=ORIENTED_EDGE('',*,*,#14926,.F.);
#21119=ORIENTED_EDGE('',*,*,#14703,.F.);
#21120=ORIENTED_EDGE('',*,*,#14920,.T.);
#21121=ORIENTED_EDGE('',*,*,#14924,.T.);
#21122=ORIENTED_EDGE('',*,*,#14927,.F.);
#21123=ORIENTED_EDGE('',*,*,#14700,.F.);
#21124=ORIENTED_EDGE('',*,*,#14927,.T.);
#21125=ORIENTED_EDGE('',*,*,#14926,.T.);
#21126=ORIENTED_EDGE('',*,*,#14928,.F.);
#21127=ORIENTED_EDGE('',*,*,#14698,.F.);
#21128=ORIENTED_EDGE('',*,*,#14928,.T.);
#21129=ORIENTED_EDGE('',*,*,#14925,.T.);
#21130=ORIENTED_EDGE('',*,*,#14921,.T.);
#21131=ORIENTED_EDGE('',*,*,#14848,.F.);
#21132=ORIENTED_EDGE('',*,*,#14929,.F.);
#21133=ORIENTED_EDGE('',*,*,#14787,.F.);
#21134=ORIENTED_EDGE('',*,*,#14929,.T.);
#21135=ORIENTED_EDGE('',*,*,#14849,.F.);
#21136=ORIENTED_EDGE('',*,*,#14825,.F.);
#26445=PLANE('',#28714);
#26446=PLANE('',#28718);
#26447=PLANE('',#28807);
#26448=PLANE('',#28810);
#26449=PLANE('',#28811);
#26450=PLANE('',#28812);
#26451=PLANE('',#28815);
#26452=PLANE('',#28818);
#26453=PLANE('',#28822);
#26454=PLANE('',#28825);
#26455=PLANE('',#28828);
#26456=PLANE('',#28829);
#26457=PLANE('',#28830);
#26458=PLANE('',#28831);
#26459=PLANE('',#28855);
#26460=PLANE('',#28906);
#26461=PLANE('',#28907);
#26462=PLANE('',#28908);
#26463=PLANE('',#28909);
#26464=PLANE('',#28911);
#26465=PLANE('',#28912);
#26466=PLANE('',#28913);
#26467=PLANE('',#28915);
#26468=PLANE('',#28917);
#26469=PLANE('',#28924);
#26470=PLANE('',#28925);
#26471=PLANE('',#28927);
#26472=PLANE('',#28929);
#27182=ADVANCED_FACE('',(#3379),#2448,.F.);
#27183=ADVANCED_FACE('',(#3380),#26445,.F.);
#27184=ADVANCED_FACE('',(#3381),#2449,.F.);
#27185=ADVANCED_FACE('',(#3382),#26446,.T.);
#27186=ADVANCED_FACE('',(#3383),#2450,.T.);
#27187=ADVANCED_FACE('',(#3384),#2451,.T.);
#27188=ADVANCED_FACE('',(#3385),#2452,.T.);
#27189=ADVANCED_FACE('',(#3386),#63,.T.);
#27190=ADVANCED_FACE('',(#3387),#2453,.T.);
#27191=ADVANCED_FACE('',(#3388),#64,.T.);
#27192=ADVANCED_FACE('',(#3389),#2454,.T.);
#27193=ADVANCED_FACE('',(#3390),#65,.T.);
#27194=ADVANCED_FACE('',(#3391),#2455,.T.);
#27195=ADVANCED_FACE('',(#3392),#55,.F.);
#27196=ADVANCED_FACE('',(#3393),#2456,.T.);
#27197=ADVANCED_FACE('',(#3394),#2457,.T.);
#27198=ADVANCED_FACE('',(#3395),#2458,.T.);
#27199=ADVANCED_FACE('',(#3396),#66,.T.);
#27200=ADVANCED_FACE('',(#3397),#2459,.T.);
#27201=ADVANCED_FACE('',(#3398),#2460,.T.);
#27202=ADVANCED_FACE('',(#3399),#2461,.T.);
#27203=ADVANCED_FACE('',(#3400),#67,.T.);
#27204=ADVANCED_FACE('',(#3401),#2462,.T.);
#27205=ADVANCED_FACE('',(#3402),#2463,.T.);
#27206=ADVANCED_FACE('',(#3403),#2464,.T.);
#27207=ADVANCED_FACE('',(#3404),#56,.F.);
#27208=ADVANCED_FACE('',(#3405),#2465,.T.);
#27209=ADVANCED_FACE('',(#3406),#68,.T.);
#27210=ADVANCED_FACE('',(#3407),#2466,.T.);
#27211=ADVANCED_FACE('',(#3408),#69,.T.);
#27212=ADVANCED_FACE('',(#3409),#2467,.T.);
#27213=ADVANCED_FACE('',(#3410),#70,.T.);
#27214=ADVANCED_FACE('',(#3411),#2468,.T.);
#27215=ADVANCED_FACE('',(#3412),#2469,.T.);
#27216=ADVANCED_FACE('',(#3413),#2470,.T.);
#27217=ADVANCED_FACE('',(#3414),#2471,.T.);
#27218=ADVANCED_FACE('',(#3415),#47,.T.);
#27219=ADVANCED_FACE('',(#3416),#48,.T.);
#27220=ADVANCED_FACE('',(#3417),#26447,.T.);
#27221=ADVANCED_FACE('',(#3418),#2472,.F.);
#27222=ADVANCED_FACE('',(#3419),#26448,.T.);
#27223=ADVANCED_FACE('',(#3420),#26449,.T.);
#27224=ADVANCED_FACE('',(#3421),#26450,.T.);
#27225=ADVANCED_FACE('',(#3422),#2473,.T.);
#27226=ADVANCED_FACE('',(#3423,#200),#26451,.T.);
#27227=ADVANCED_FACE('',(#3424),#2474,.T.);
#27228=ADVANCED_FACE('',(#3425),#26452,.T.);
#27229=ADVANCED_FACE('',(#3426),#2475,.T.);
#27230=ADVANCED_FACE('',(#3427),#26453,.T.);
#27231=ADVANCED_FACE('',(#3428),#2476,.F.);
#27232=ADVANCED_FACE('',(#3429),#26454,.T.);
#27233=ADVANCED_FACE('',(#3430),#2477,.T.);
#27234=ADVANCED_FACE('',(#3431),#26455,.T.);
#27235=ADVANCED_FACE('',(#3432),#26456,.T.);
#27236=ADVANCED_FACE('',(#3433),#26457,.T.);
#27237=ADVANCED_FACE('',(#3434),#26458,.F.);
#27238=ADVANCED_FACE('',(#3435),#2478,.T.);
#27239=ADVANCED_FACE('',(#3436),#71,.T.);
#27240=ADVANCED_FACE('',(#3437),#2479,.T.);
#27241=ADVANCED_FACE('',(#3438),#2480,.T.);
#27242=ADVANCED_FACE('',(#3439),#2481,.T.);
#27243=ADVANCED_FACE('',(#3440),#49,.T.);
#27244=ADVANCED_FACE('',(#3441),#72,.T.);
#27245=ADVANCED_FACE('',(#3442),#2482,.T.);
#27246=ADVANCED_FACE('',(#3443),#50,.T.);
#27247=ADVANCED_FACE('',(#3444),#2483,.T.);
#27248=ADVANCED_FACE('',(#3445),#26459,.T.);
#27249=ADVANCED_FACE('',(#3446),#2484,.T.);
#27250=ADVANCED_FACE('',(#3447),#73,.T.);
#27251=ADVANCED_FACE('',(#3448),#2485,.T.);
#27252=ADVANCED_FACE('',(#3449),#57,.F.);
#27253=ADVANCED_FACE('',(#3450),#2486,.T.);
#27254=ADVANCED_FACE('',(#3451),#74,.T.);
#27255=ADVANCED_FACE('',(#3452),#75,.T.);
#27256=ADVANCED_FACE('',(#3453),#2487,.T.);
#27257=ADVANCED_FACE('',(#3454),#2488,.T.);
#27258=ADVANCED_FACE('',(#3455),#76,.T.);
#27259=ADVANCED_FACE('',(#3456),#2489,.T.);
#27260=ADVANCED_FACE('',(#3457),#2490,.T.);
#27261=ADVANCED_FACE('',(#3458),#2491,.T.);
#27262=ADVANCED_FACE('',(#3459),#2492,.T.);
#27263=ADVANCED_FACE('',(#3460),#2493,.T.);
#27264=ADVANCED_FACE('',(#3461),#77,.T.);
#27265=ADVANCED_FACE('',(#3462),#2494,.T.);
#27266=ADVANCED_FACE('',(#3463),#2495,.T.);
#27267=ADVANCED_FACE('',(#3464),#78,.T.);
#27268=ADVANCED_FACE('',(#3465),#2496,.T.);
#27269=ADVANCED_FACE('',(#3466),#58,.F.);
#27270=ADVANCED_FACE('',(#3467),#2497,.T.);
#27271=ADVANCED_FACE('',(#3468),#26460,.T.);
#27272=ADVANCED_FACE('',(#3469),#26461,.T.);
#27273=ADVANCED_FACE('',(#3470),#26462,.T.);
#27274=ADVANCED_FACE('',(#3471),#26463,.T.);
#27275=ADVANCED_FACE('',(#3472),#2498,.F.);
#27276=ADVANCED_FACE('',(#3473),#26464,.T.);
#27277=ADVANCED_FACE('',(#3474),#26465,.T.);
#27278=ADVANCED_FACE('',(#3475),#26466,.T.);
#27279=ADVANCED_FACE('',(#3476),#2499,.T.);
#27280=ADVANCED_FACE('',(#3477,#201),#26467,.T.);
#27281=ADVANCED_FACE('',(#3478),#2500,.T.);
#27282=ADVANCED_FACE('',(#3479),#26468,.T.);
#27283=ADVANCED_FACE('',(#3480),#2501,.T.);
#27284=ADVANCED_FACE('',(#3481),#2502,.F.);
#27285=ADVANCED_FACE('',(#3482),#2503,.F.);
#27286=ADVANCED_FACE('',(#3483),#26469,.T.);
#27287=ADVANCED_FACE('',(#3484),#26470,.T.);
#27288=ADVANCED_FACE('',(#3485),#26471,.T.);
#27289=ADVANCED_FACE('',(#3486),#2504,.F.);
#27290=ADVANCED_FACE('',(#3487),#26472,.T.);
#27291=ADVANCED_FACE('',(#3488),#2505,.T.);
#28083=CLOSED_SHELL('',(#27182,#27183,#27184,#27185,#27186,#27187,#27188,
#27189,#27190,#27191,#27192,#27193,#27194,#27195,#27196,#27197,#27198,#27199,
#27200,#27201,#27202,#27203,#27204,#27205,#27206,#27207,#27208,#27209,#27210,
#27211,#27212,#27213,#27214,#27215,#27216,#27217,#27218,#27219,#27220,#27221,
#27222,#27223,#27224,#27225,#27226,#27227,#27228,#27229,#27230,#27231,#27232,
#27233,#27234,#27235,#27236,#27237,#27238,#27239,#27240,#27241,#27242,#27243,
#27244,#27245,#27246,#27247,#27248,#27249,#27250,#27251,#27252,#27253,#27254,
#27255,#27256,#27257,#27258,#27259,#27260,#27261,#27262,#27263,#27264,#27265,
#27266,#27267,#27268,#27269,#27270,#27271,#27272,#27273,#27274,#27275,#27276,
#27277,#27278,#27279,#27280,#27281,#27282,#27283,#27284,#27285,#27286,#27287,
#27288,#27289,#27290,#27291));
#28710=AXIS2_PLACEMENT_3D('',#124428,#31764,#31765);
#28711=AXIS2_PLACEMENT_3D('',#124429,#31766,#31767);
#28712=AXIS2_PLACEMENT_3D('',#124431,#31768,#31769);
#28713=AXIS2_PLACEMENT_3D('',#124434,#31771,#31772);
#28714=AXIS2_PLACEMENT_3D('',#124435,#31773,#31774);
#28715=AXIS2_PLACEMENT_3D('',#124436,#31775,#31776);
#28716=AXIS2_PLACEMENT_3D('',#124438,#31777,#31778);
#28717=AXIS2_PLACEMENT_3D('',#124441,#31780,#31781);
#28718=AXIS2_PLACEMENT_3D('',#124442,#31782,#31783);
#28719=AXIS2_PLACEMENT_3D('',#124443,#31784,#31785);
#28720=AXIS2_PLACEMENT_3D('',#124448,#31787,#31788);
#28721=AXIS2_PLACEMENT_3D('',#124451,#31790,#31791);
#28722=AXIS2_PLACEMENT_3D('',#124452,#31792,#31793);
#28723=AXIS2_PLACEMENT_3D('',#124456,#31795,#31796);
#28724=AXIS2_PLACEMENT_3D('',#124458,#31798,#31799);
#28725=AXIS2_PLACEMENT_3D('',#124461,#31800,#31801);
#28726=AXIS2_PLACEMENT_3D('',#124465,#31803,#31804);
#28727=AXIS2_PLACEMENT_3D('',#124467,#31806,#31807);
#28728=AXIS2_PLACEMENT_3D('',#124470,#31808,#31809);
#28729=AXIS2_PLACEMENT_3D('',#124471,#31810,#31811);
#28730=AXIS2_PLACEMENT_3D('',#124472,#31812,#31813);
#28731=AXIS2_PLACEMENT_3D('',#124473,#31814,#31815);
#28732=AXIS2_PLACEMENT_3D('',#124476,#31816,#31817);
#28733=AXIS2_PLACEMENT_3D('',#124479,#31820,#31821);
#28734=AXIS2_PLACEMENT_3D('',#124482,#31822,#31823);
#28735=AXIS2_PLACEMENT_3D('',#124483,#31824,#31825);
#28736=AXIS2_PLACEMENT_3D('',#124484,#31826,#31827);
#28737=AXIS2_PLACEMENT_3D('',#124485,#31828,#31829);
#28738=AXIS2_PLACEMENT_3D('',#124488,#31830,#31831);
#28739=AXIS2_PLACEMENT_3D('',#124491,#31834,#31835);
#28740=AXIS2_PLACEMENT_3D('',#124494,#31836,#31837);
#28741=AXIS2_PLACEMENT_3D('',#124495,#31838,#31839);
#28742=AXIS2_PLACEMENT_3D('',#124496,#31840,#31841);
#28743=AXIS2_PLACEMENT_3D('',#124497,#31842,#31843);
#28744=AXIS2_PLACEMENT_3D('',#124500,#31844,#31845);
#28745=AXIS2_PLACEMENT_3D('',#124514,#31848,#31849);
#28746=AXIS2_PLACEMENT_3D('',#124515,#31850,#31851);
#28747=AXIS2_PLACEMENT_3D('',#124516,#31852,#31853);
#28748=AXIS2_PLACEMENT_3D('',#124517,#31854,#31855);
#28749=AXIS2_PLACEMENT_3D('',#124522,#31858,#31859);
#28750=AXIS2_PLACEMENT_3D('',#124523,#31860,#31861);
#28751=AXIS2_PLACEMENT_3D('',#124528,#31864,#31865);
#28752=AXIS2_PLACEMENT_3D('',#124529,#31866,#31867);
#28753=AXIS2_PLACEMENT_3D('',#124533,#31869,#31870);
#28754=AXIS2_PLACEMENT_3D('',#124535,#31872,#31873);
#28755=AXIS2_PLACEMENT_3D('',#124538,#31874,#31875);
#28756=AXIS2_PLACEMENT_3D('',#124539,#31876,#31877);
#28757=AXIS2_PLACEMENT_3D('',#124540,#31878,#31879);
#28758=AXIS2_PLACEMENT_3D('',#124541,#31880,#31881);
#28759=AXIS2_PLACEMENT_3D('',#124546,#31884,#31885);
#28760=AXIS2_PLACEMENT_3D('',#124547,#31886,#31887);
#28761=AXIS2_PLACEMENT_3D('',#124550,#31890,#31891);
#28762=AXIS2_PLACEMENT_3D('',#124554,#31893,#31894);
#28763=AXIS2_PLACEMENT_3D('',#124556,#31896,#31897);
#28764=AXIS2_PLACEMENT_3D('',#124559,#31898,#31899);
#28765=AXIS2_PLACEMENT_3D('',#124560,#31900,#31901);
#28766=AXIS2_PLACEMENT_3D('',#124561,#31902,#31903);
#28767=AXIS2_PLACEMENT_3D('',#124562,#31904,#31905);
#28768=AXIS2_PLACEMENT_3D('',#124567,#31908,#31909);
#28769=AXIS2_PLACEMENT_3D('',#124568,#31910,#31911);
#28770=AXIS2_PLACEMENT_3D('',#124572,#31913,#31914);
#28771=AXIS2_PLACEMENT_3D('',#124574,#31916,#31917);
#28772=AXIS2_PLACEMENT_3D('',#124578,#31919,#31920);
#28773=AXIS2_PLACEMENT_3D('',#124591,#31922,#31923);
#28774=AXIS2_PLACEMENT_3D('',#124592,#31924,#31925);
#28775=AXIS2_PLACEMENT_3D('',#124593,#31926,#31927);
#28776=AXIS2_PLACEMENT_3D('',#124594,#31928,#31929);
#28777=AXIS2_PLACEMENT_3D('',#124597,#31930,#31931);
#28778=AXIS2_PLACEMENT_3D('',#124600,#31934,#31935);
#28779=AXIS2_PLACEMENT_3D('',#124603,#31936,#31937);
#28780=AXIS2_PLACEMENT_3D('',#124604,#31938,#31939);
#28781=AXIS2_PLACEMENT_3D('',#124605,#31940,#31941);
#28782=AXIS2_PLACEMENT_3D('',#124606,#31942,#31943);
#28783=AXIS2_PLACEMENT_3D('',#124609,#31944,#31945);
#28784=AXIS2_PLACEMENT_3D('',#124612,#31948,#31949);
#28785=AXIS2_PLACEMENT_3D('',#124615,#31950,#31951);
#28786=AXIS2_PLACEMENT_3D('',#124616,#31952,#31953);
#28787=AXIS2_PLACEMENT_3D('',#124617,#31954,#31955);
#28788=AXIS2_PLACEMENT_3D('',#124618,#31956,#31957);
#28789=AXIS2_PLACEMENT_3D('',#124621,#31958,#31959);
#28790=AXIS2_PLACEMENT_3D('',#124624,#31962,#31963);
#28791=AXIS2_PLACEMENT_3D('',#124627,#31964,#31965);
#28792=AXIS2_PLACEMENT_3D('',#124628,#31966,#31967);
#28793=AXIS2_PLACEMENT_3D('',#124629,#31968,#31969);
#28794=AXIS2_PLACEMENT_3D('',#124630,#31970,#31971);
#28795=AXIS2_PLACEMENT_3D('',#124633,#31972,#31973);
#28796=AXIS2_PLACEMENT_3D('',#124636,#31976,#31977);
#28797=AXIS2_PLACEMENT_3D('',#124639,#31978,#31979);
#28798=AXIS2_PLACEMENT_3D('',#124642,#31981,#31982);
#28799=AXIS2_PLACEMENT_3D('',#124644,#31984,#31985);
#28800=AXIS2_PLACEMENT_3D('',#124648,#31987,#31988);
#28801=AXIS2_PLACEMENT_3D('',#124650,#31990,#31991);
#28802=AXIS2_PLACEMENT_3D('',#124653,#31993,#31994);
#28803=AXIS2_PLACEMENT_3D('',#124655,#31996,#31997);
#28804=AXIS2_PLACEMENT_3D('',#124656,#31998,#31999);
#28805=AXIS2_PLACEMENT_3D('',#124657,#32000,#32001);
#28806=AXIS2_PLACEMENT_3D('',#124658,#32002,#32003);
#28807=AXIS2_PLACEMENT_3D('',#124659,#32004,#32005);
#28808=AXIS2_PLACEMENT_3D('',#124665,#32009,#32010);
#28809=AXIS2_PLACEMENT_3D('',#124668,#32012,#32013);
#28810=AXIS2_PLACEMENT_3D('',#124669,#32014,#32015);
#28811=AXIS2_PLACEMENT_3D('',#124673,#32018,#32019);
#28812=AXIS2_PLACEMENT_3D('',#124677,#32022,#32023);
#28813=AXIS2_PLACEMENT_3D('',#124681,#32026,#32027);
#28814=AXIS2_PLACEMENT_3D('',#124684,#32029,#32030);
#28815=AXIS2_PLACEMENT_3D('',#124685,#32031,#32032);
#28816=AXIS2_PLACEMENT_3D('',#124689,#32035,#32036);
#28817=AXIS2_PLACEMENT_3D('',#124692,#32038,#32039);
#28818=AXIS2_PLACEMENT_3D('',#124693,#32040,#32041);
#28819=AXIS2_PLACEMENT_3D('',#124697,#32044,#32045);
#28820=AXIS2_PLACEMENT_3D('',#124701,#32047,#32048);
#28821=AXIS2_PLACEMENT_3D('',#124704,#32050,#32051);
#28822=AXIS2_PLACEMENT_3D('',#124705,#32052,#32053);
#28823=AXIS2_PLACEMENT_3D('',#124709,#32056,#32057);
#28824=AXIS2_PLACEMENT_3D('',#124712,#32059,#32060);
#28825=AXIS2_PLACEMENT_3D('',#124713,#32061,#32062);
#28826=AXIS2_PLACEMENT_3D('',#124721,#32067,#32068);
#28827=AXIS2_PLACEMENT_3D('',#124724,#32070,#32071);
#28828=AXIS2_PLACEMENT_3D('',#124725,#32072,#32073);
#28829=AXIS2_PLACEMENT_3D('',#124729,#32076,#32077);
#28830=AXIS2_PLACEMENT_3D('',#124733,#32080,#32081);
#28831=AXIS2_PLACEMENT_3D('',#124737,#32084,#32085);
#28832=AXIS2_PLACEMENT_3D('',#124738,#32086,#32087);
#28833=AXIS2_PLACEMENT_3D('',#124740,#32088,#32089);
#28834=AXIS2_PLACEMENT_3D('',#124757,#32091,#32092);
#28835=AXIS2_PLACEMENT_3D('',#124759,#32093,#32094);
#28836=AXIS2_PLACEMENT_3D('',#124781,#32095,#32096);
#28837=AXIS2_PLACEMENT_3D('',#124782,#32097,#32098);
#28838=AXIS2_PLACEMENT_3D('',#124784,#32099,#32100);
#28839=AXIS2_PLACEMENT_3D('',#124786,#32102,#32103);
#28840=AXIS2_PLACEMENT_3D('',#124787,#32104,#32105);
#28841=AXIS2_PLACEMENT_3D('',#124789,#32106,#32107);
#28842=AXIS2_PLACEMENT_3D('',#124791,#32109,#32110);
#28843=AXIS2_PLACEMENT_3D('',#124793,#32111,#32112);
#28844=AXIS2_PLACEMENT_3D('',#124795,#32114,#32115);
#28845=AXIS2_PLACEMENT_3D('',#124796,#32116,#32117);
#28846=AXIS2_PLACEMENT_3D('',#124799,#32118,#32119);
#28847=AXIS2_PLACEMENT_3D('',#124823,#32120,#32121);
#28848=AXIS2_PLACEMENT_3D('',#124838,#32122,#32123);
#28849=AXIS2_PLACEMENT_3D('',#124841,#32125,#32126);
#28850=AXIS2_PLACEMENT_3D('',#124843,#32128,#32129);
#28851=AXIS2_PLACEMENT_3D('',#124844,#32130,#32131);
#28852=AXIS2_PLACEMENT_3D('',#124845,#32132,#32133);
#28853=AXIS2_PLACEMENT_3D('',#124848,#32135,#32136);
#28854=AXIS2_PLACEMENT_3D('',#124849,#32137,#32138);
#28855=AXIS2_PLACEMENT_3D('',#124850,#32139,#32140);
#28856=AXIS2_PLACEMENT_3D('',#124854,#32142,#32143);
#28857=AXIS2_PLACEMENT_3D('',#124858,#32145,#32146);
#28858=AXIS2_PLACEMENT_3D('',#124866,#32150,#32151);
#28859=AXIS2_PLACEMENT_3D('',#124878,#32157,#32158);
#28860=AXIS2_PLACEMENT_3D('',#124886,#32162,#32163);
#28861=AXIS2_PLACEMENT_3D('',#124889,#32165,#32166);
#28862=AXIS2_PLACEMENT_3D('',#124890,#32167,#32168);
#28863=AXIS2_PLACEMENT_3D('',#124892,#32169,#32170);
#28864=AXIS2_PLACEMENT_3D('',#124895,#32172,#32173);
#28865=AXIS2_PLACEMENT_3D('',#124896,#32174,#32175);
#28866=AXIS2_PLACEMENT_3D('',#124897,#32176,#32177);
#28867=AXIS2_PLACEMENT_3D('',#124898,#32178,#32179);
#28868=AXIS2_PLACEMENT_3D('',#124899,#32180,#32181);
#28869=AXIS2_PLACEMENT_3D('',#124900,#32182,#32183);
#28870=AXIS2_PLACEMENT_3D('',#124910,#32184,#32185);
#28871=AXIS2_PLACEMENT_3D('',#124911,#32186,#32187);
#28872=AXIS2_PLACEMENT_3D('',#124912,#32188,#32189);
#28873=AXIS2_PLACEMENT_3D('',#124913,#32190,#32191);
#28874=AXIS2_PLACEMENT_3D('',#124914,#32192,#32193);
#28875=AXIS2_PLACEMENT_3D('',#124915,#32194,#32195);
#28876=AXIS2_PLACEMENT_3D('',#124916,#32196,#32197);
#28877=AXIS2_PLACEMENT_3D('',#124917,#32198,#32199);
#28878=AXIS2_PLACEMENT_3D('',#124918,#32200,#32201);
#28879=AXIS2_PLACEMENT_3D('',#124919,#32202,#32203);
#28880=AXIS2_PLACEMENT_3D('',#124920,#32204,#32205);
#28881=AXIS2_PLACEMENT_3D('',#124921,#32206,#32207);
#28882=AXIS2_PLACEMENT_3D('',#124922,#32208,#32209);
#28883=AXIS2_PLACEMENT_3D('',#124923,#32210,#32211);
#28884=AXIS2_PLACEMENT_3D('',#124927,#32213,#32214);
#28885=AXIS2_PLACEMENT_3D('',#124928,#32215,#32216);
#28886=AXIS2_PLACEMENT_3D('',#124929,#32217,#32218);
#28887=AXIS2_PLACEMENT_3D('',#124931,#32219,#32220);
#28888=AXIS2_PLACEMENT_3D('',#124933,#32222,#32223);
#28889=AXIS2_PLACEMENT_3D('',#124935,#32225,#32226);
#28890=AXIS2_PLACEMENT_3D('',#124939,#32228,#32229);
#28891=AXIS2_PLACEMENT_3D('',#124940,#32230,#32231);
#28892=AXIS2_PLACEMENT_3D('',#124941,#32232,#32233);
#28893=AXIS2_PLACEMENT_3D('',#124943,#32234,#32235);
#28894=AXIS2_PLACEMENT_3D('',#124944,#32236,#32237);
#28895=AXIS2_PLACEMENT_3D('',#124945,#32238,#32239);
#28896=AXIS2_PLACEMENT_3D('',#124947,#32241,#32242);
#28897=AXIS2_PLACEMENT_3D('',#124950,#32244,#32245);
#28898=AXIS2_PLACEMENT_3D('',#124951,#32246,#32247);
#28899=AXIS2_PLACEMENT_3D('',#124953,#32248,#32249);
#28900=AXIS2_PLACEMENT_3D('',#124954,#32250,#32251);
#28901=AXIS2_PLACEMENT_3D('',#124955,#32252,#32253);
#28902=AXIS2_PLACEMENT_3D('',#124957,#32254,#32255);
#28903=AXIS2_PLACEMENT_3D('',#124969,#32257,#32258);
#28904=AXIS2_PLACEMENT_3D('',#124970,#32259,#32260);
#28905=AXIS2_PLACEMENT_3D('',#124971,#32261,#32262);
#28906=AXIS2_PLACEMENT_3D('',#124973,#32264,#32265);
#28907=AXIS2_PLACEMENT_3D('',#124975,#32267,#32268);
#28908=AXIS2_PLACEMENT_3D('',#124977,#32270,#32271);
#28909=AXIS2_PLACEMENT_3D('',#124979,#32273,#32274);
#28910=AXIS2_PLACEMENT_3D('',#124981,#32276,#32277);
#28911=AXIS2_PLACEMENT_3D('',#124983,#32279,#32280);
#28912=AXIS2_PLACEMENT_3D('',#124985,#32282,#32283);
#28913=AXIS2_PLACEMENT_3D('',#124987,#32285,#32286);
#28914=AXIS2_PLACEMENT_3D('',#124989,#32288,#32289);
#28915=AXIS2_PLACEMENT_3D('',#124991,#32291,#32292);
#28916=AXIS2_PLACEMENT_3D('',#124993,#32294,#32295);
#28917=AXIS2_PLACEMENT_3D('',#124995,#32297,#32298);
#28918=AXIS2_PLACEMENT_3D('',#124997,#32300,#32301);
#28919=AXIS2_PLACEMENT_3D('',#125001,#32303,#32304);
#28920=AXIS2_PLACEMENT_3D('',#125003,#32306,#32307);
#28921=AXIS2_PLACEMENT_3D('',#125006,#32309,#32310);
#28922=AXIS2_PLACEMENT_3D('',#125007,#32311,#32312);
#28923=AXIS2_PLACEMENT_3D('',#125008,#32313,#32314);
#28924=AXIS2_PLACEMENT_3D('',#125009,#32315,#32316);
#28925=AXIS2_PLACEMENT_3D('',#125010,#32317,#32318);
#28926=AXIS2_PLACEMENT_3D('',#125015,#32321,#32322);
#28927=AXIS2_PLACEMENT_3D('',#125016,#32323,#32324);
#28928=AXIS2_PLACEMENT_3D('',#125018,#32326,#32327);
#28929=AXIS2_PLACEMENT_3D('',#125020,#32329,#32330);
#28930=AXIS2_PLACEMENT_3D('',#125022,#32332,#32333);
#31764=DIRECTION('axis',(0.,0.,1.));
#31765=DIRECTION('refdir',(1.,0.,0.));
#31766=DIRECTION('center_axis',(1.,6.57957785206009E-13,0.));
#31767=DIRECTION('ref_axis',(0.,0.,1.));
#31768=DIRECTION('center_axis',(1.,6.58286732145141E-13,0.));
#31769=DIRECTION('ref_axis',(0.,0.,1.));
#31770=DIRECTION('',(1.,6.57957785206009E-13,0.));
#31771=DIRECTION('center_axis',(-1.,3.28954970259306E-16,0.));
#31772=DIRECTION('ref_axis',(0.,0.,1.));
#31773=DIRECTION('center_axis',(-1.,-6.58286732145141E-13,0.));
#31774=DIRECTION('ref_axis',(0.,0.,1.));
#31775=DIRECTION('center_axis',(0.999999999362884,-3.56963971004376E-5,
0.));
#31776=DIRECTION('ref_axis',(0.,0.,1.));
#31777=DIRECTION('center_axis',(0.999999999362884,-3.56963971007665E-5,
0.));
#31778=DIRECTION('ref_axis',(0.,0.,1.));
#31779=DIRECTION('',(0.999999999362884,-3.56963971004376E-5,0.));
#31780=DIRECTION('center_axis',(0.999999999362884,-3.56963971007665E-5,
0.));
#31781=DIRECTION('ref_axis',(0.,0.,1.));
#31782=DIRECTION('center_axis',(-0.999999999362884,3.56963971007665E-5,
0.));
#31783=DIRECTION('ref_axis',(0.,0.,1.));
#31784=DIRECTION('center_axis',(-0.999999999362884,3.56963971010297E-5,
0.));
#31785=DIRECTION('ref_axis',(-2.52411644540658E-5,-0.707106780736035,0.707106781186551));
#31786=DIRECTION('',(0.999999999362884,-3.56963971010297E-5,0.));
#31787=DIRECTION('center_axis',(-0.999999999362884,3.56963970959969E-5,
0.));
#31788=DIRECTION('ref_axis',(-3.56963970959969E-5,-0.999999999362884,0.));
#31789=DIRECTION('',(-0.999999999362884,3.56963971010297E-5,0.));
#31790=DIRECTION('center_axis',(0.970304361397857,0.24188725938399,0.));
#31791=DIRECTION('ref_axis',(0.24188725938399,-0.970304361397857,0.));
#31792=DIRECTION('center_axis',(0.999999999840721,-1.7848198553344E-5,0.));
#31793=DIRECTION('ref_axis',(-1.26205822290334E-5,-0.707106781073918,0.70710678118655));
#31794=DIRECTION('',(0.999999999840721,-1.7848198553344E-5,0.));
#31795=DIRECTION('center_axis',(-0.999999999840721,1.78481985546597E-5,
0.));
#31796=DIRECTION('ref_axis',(-1.78481985546597E-5,-0.999999999840721,0.));
#31797=DIRECTION('',(-0.999999999840721,1.7848198553344E-5,0.));
#31798=DIRECTION('center_axis',(0.,-1.,0.));
#31799=DIRECTION('ref_axis',(0.707106781186548,0.,0.707106781186548));
#31800=DIRECTION('center_axis',(0.,-1.,0.));
#31801=DIRECTION('ref_axis',(1.,0.,0.));
#31802=DIRECTION('',(0.,-1.,0.));
#31803=DIRECTION('center_axis',(0.,1.,0.));
#31804=DIRECTION('ref_axis',(0.,0.,1.));
#31805=DIRECTION('',(0.,1.,0.));
#31806=DIRECTION('center_axis',(0.,0.,-1.));
#31807=DIRECTION('ref_axis',(-1.,0.,0.));
#31808=DIRECTION('center_axis',(-1.,0.,0.));
#31809=DIRECTION('ref_axis',(0.,0.,1.));
#31810=DIRECTION('center_axis',(0.,0.,-1.));
#31811=DIRECTION('ref_axis',(-0.707106781186545,-0.70710678118655,0.));
#31812=DIRECTION('center_axis',(0.,0.,1.));
#31813=DIRECTION('ref_axis',(-0.707106781186545,-0.70710678118655,0.));
#31814=DIRECTION('center_axis',(1.,0.,0.));
#31815=DIRECTION('ref_axis',(0.,0.707106781186548,0.707106781186548));
#31816=DIRECTION('center_axis',(-1.,0.,0.));
#31817=DIRECTION('ref_axis',(0.,0.,1.));
#31818=DIRECTION('',(-1.,0.,0.));
#31819=DIRECTION('',(1.,0.,0.));
#31820=DIRECTION('center_axis',(0.,0.,-1.));
#31821=DIRECTION('ref_axis',(-1.,0.,0.));
#31822=DIRECTION('center_axis',(-0.707106781186545,0.70710678118655,0.));
#31823=DIRECTION('ref_axis',(0.,0.,1.));
#31824=DIRECTION('center_axis',(0.,0.,1.));
#31825=DIRECTION('ref_axis',(0.382683432365091,0.923879532511286,0.));
#31826=DIRECTION('center_axis',(0.,0.,-1.));
#31827=DIRECTION('ref_axis',(0.382683432365091,0.923879532511286,0.));
#31828=DIRECTION('center_axis',(0.707106781186548,-0.707106781186547,0.));
#31829=DIRECTION('ref_axis',(0.5,0.500000000000001,0.707106781186547));
#31830=DIRECTION('center_axis',(-0.707106781186548,0.707106781186548,0.));
#31831=DIRECTION('ref_axis',(0.,0.,1.));
#31832=DIRECTION('',(-0.707106781186548,0.707106781186547,0.));
#31833=DIRECTION('',(0.707106781186548,-0.707106781186547,0.));
#31834=DIRECTION('center_axis',(0.,0.,-1.));
#31835=DIRECTION('ref_axis',(-1.,0.,0.));
#31836=DIRECTION('center_axis',(0.,1.,0.));
#31837=DIRECTION('ref_axis',(0.,0.,1.));
#31838=DIRECTION('center_axis',(0.,0.,1.));
#31839=DIRECTION('ref_axis',(0.923879532511287,0.38268343236509,0.));
#31840=DIRECTION('center_axis',(0.,0.,-1.));
#31841=DIRECTION('ref_axis',(0.923879532511287,0.38268343236509,0.));
#31842=DIRECTION('center_axis',(-3.28954970259306E-16,-1.,0.));
#31843=DIRECTION('ref_axis',(0.707106781186548,-2.32606290175374E-16,0.707106781186548));
#31844=DIRECTION('center_axis',(0.,1.,0.));
#31845=DIRECTION('ref_axis',(0.,0.,1.));
#31846=DIRECTION('',(3.28954970259306E-16,1.,0.));
#31847=DIRECTION('',(-3.28954970259306E-16,-1.,0.));
#31848=DIRECTION('center_axis',(1.,0.,0.));
#31849=DIRECTION('ref_axis',(0.,0.,1.));
#31850=DIRECTION('center_axis',(0.,0.,1.));
#31851=DIRECTION('ref_axis',(0.707106781186546,-0.707106781186549,0.));
#31852=DIRECTION('center_axis',(0.,0.,-1.));
#31853=DIRECTION('ref_axis',(0.707106781186547,-0.707106781186548,0.));
#31854=DIRECTION('center_axis',(-1.,0.,0.));
#31855=DIRECTION('ref_axis',(0.,-0.707106781186548,0.707106781186548));
#31856=DIRECTION('',(1.,0.,0.));
#31857=DIRECTION('',(-1.,0.,0.));
#31858=DIRECTION('center_axis',(0.92387953251129,-0.382683432365083,0.));
#31859=DIRECTION('ref_axis',(0.382683432365083,0.92387953251129,0.));
#31860=DIRECTION('center_axis',(-0.707106781186548,0.707106781186547,0.));
#31861=DIRECTION('ref_axis',(-0.499999999999999,-0.499999999999999,0.707106781186549));
#31862=DIRECTION('',(0.707106781186548,-0.707106781186547,0.));
#31863=DIRECTION('',(-0.707106781186548,0.707106781186547,0.));
#31864=DIRECTION('center_axis',(0.382683432365083,-0.92387953251129,0.));
#31865=DIRECTION('ref_axis',(0.92387953251129,0.382683432365083,0.));
#31866=DIRECTION('center_axis',(0.,1.,0.));
#31867=DIRECTION('ref_axis',(-0.707106781186551,0.,0.707106781186544));
#31868=DIRECTION('',(0.,1.,0.));
#31869=DIRECTION('center_axis',(0.,-1.,0.));
#31870=DIRECTION('ref_axis',(0.,0.,1.));
#31871=DIRECTION('',(0.,-1.,0.));
#31872=DIRECTION('center_axis',(0.,0.,-1.));
#31873=DIRECTION('ref_axis',(-1.,0.,0.));
#31874=DIRECTION('center_axis',(0.88294759285893,-0.469471562785885,0.));
#31875=DIRECTION('ref_axis',(0.,0.,1.));
#31876=DIRECTION('center_axis',(0.,0.,-1.));
#31877=DIRECTION('ref_axis',(0.857167300702112,0.515038074910055,0.));
#31878=DIRECTION('center_axis',(0.,0.,1.));
#31879=DIRECTION('ref_axis',(0.857167300702112,0.515038074910055,0.));
#31880=DIRECTION('center_axis',(-0.882947592858928,0.46947156278589,0.));
#31881=DIRECTION('ref_axis',(-0.331966525620151,-0.624338230342891,0.707106781186542));
#31882=DIRECTION('',(0.882947592858928,-0.46947156278589,0.));
#31883=DIRECTION('',(-0.882947592858928,0.46947156278589,0.));
#31884=DIRECTION('center_axis',(0.970295726275989,-0.241921895599697,0.));
#31885=DIRECTION('ref_axis',(-0.241921895599697,-0.970295726275989,0.));
#31886=DIRECTION('center_axis',(-1.,0.,0.));
#31887=DIRECTION('ref_axis',(0.,-0.707106781186548,0.707106781186548));
#31888=DIRECTION('',(1.,0.,0.));
#31889=DIRECTION('',(-1.,0.,0.));
#31890=DIRECTION('center_axis',(-0.882964350739721,-0.469440044438886,0.));
#31891=DIRECTION('ref_axis',(0.331944238783253,-0.624350079954038,0.707106781186543));
#31892=DIRECTION('',(-0.882964350739721,-0.469440044438886,0.));
#31893=DIRECTION('center_axis',(0.882964350739719,0.46944004443889,0.));
#31894=DIRECTION('ref_axis',(0.,0.,1.));
#31895=DIRECTION('',(0.882964350739721,0.469440044438886,0.));
#31896=DIRECTION('center_axis',(0.,0.,-1.));
#31897=DIRECTION('ref_axis',(-1.,0.,0.));
#31898=DIRECTION('center_axis',(3.56963971004376E-5,0.999999999362884,0.));
#31899=DIRECTION('ref_axis',(0.,0.,1.));
#31900=DIRECTION('center_axis',(0.,0.,-1.));
#31901=DIRECTION('ref_axis',(-0.857148915152355,0.51506867236626,0.));
#31902=DIRECTION('center_axis',(0.,0.,1.));
#31903=DIRECTION('ref_axis',(-0.857148915152355,0.51506867236626,0.));
#31904=DIRECTION('center_axis',(-3.56963971014961E-5,-0.999999999362884,
0.));
#31905=DIRECTION('ref_axis',(0.707106780736038,-2.52411644543957E-5,0.707106781186548));
#31906=DIRECTION('',(3.56963971014961E-5,0.999999999362884,0.));
#31907=DIRECTION('',(-3.56963971014961E-5,-0.999999999362884,0.));
#31908=DIRECTION('center_axis',(0.382716411291948,0.9238658715029,0.));
#31909=DIRECTION('ref_axis',(-0.9238658715029,0.382716411291948,0.));
#31910=DIRECTION('center_axis',(-0.707132021900493,-0.707081539571584,0.));
#31911=DIRECTION('ref_axis',(0.499982151482891,-0.500017847879993,0.707106781186548));
#31912=DIRECTION('',(-0.707132021900493,-0.707081539571584,0.));
#31913=DIRECTION('center_axis',(0.923893192342431,0.382650452950617,-6.50651058246798E-15));
#31914=DIRECTION('ref_axis',(-0.382650452950617,0.923893192342431,1.57081060919186E-14));
#31915=DIRECTION('',(0.707132021900493,0.707081539571584,0.));
#31916=DIRECTION('center_axis',(-0.999999999362884,3.5696397100931E-5,0.));
#31917=DIRECTION('ref_axis',(-2.52411644539961E-5,-0.707106780736038,0.707106781186548));
#31918=DIRECTION('',(-0.999999999362884,3.5696397100931E-5,0.));
#31919=DIRECTION('center_axis',(0.999999999362884,-3.56963971004377E-5,
0.));
#31920=DIRECTION('ref_axis',(0.,0.,1.));
#31921=DIRECTION('',(0.999999999362884,-3.5696397100931E-5,0.));
#31922=DIRECTION('center_axis',(-3.56963971048783E-5,-0.999999999362884,
0.));
#31923=DIRECTION('ref_axis',(0.,0.,1.));
#31924=DIRECTION('center_axis',(0.,0.,1.));
#31925=DIRECTION('ref_axis',(-0.707132021900492,-0.707081539571584,0.));
#31926=DIRECTION('center_axis',(0.,0.,-1.));
#31927=DIRECTION('ref_axis',(-0.707132021900492,-0.707081539571584,0.));
#31928=DIRECTION('center_axis',(3.56963971007665E-5,0.999999999362884,0.));
#31929=DIRECTION('ref_axis',(-0.707106780736035,2.52411644538797E-5,0.707106781186551));
#31930=DIRECTION('center_axis',(-3.56963971004377E-5,-0.999999999362884,
0.));
#31931=DIRECTION('ref_axis',(0.,0.,1.));
#31932=DIRECTION('',(-3.56963971007665E-5,-0.999999999362884,0.));
#31933=DIRECTION('',(3.56963971007665E-5,0.999999999362884,0.));
#31934=DIRECTION('center_axis',(0.,0.,-1.));
#31935=DIRECTION('ref_axis',(-1.,0.,0.));
#31936=DIRECTION('center_axis',(-0.707132021900495,-0.707081539571582,0.));
#31937=DIRECTION('ref_axis',(0.,0.,1.));
#31938=DIRECTION('center_axis',(0.,0.,1.));
#31939=DIRECTION('ref_axis',(-0.923865871502902,0.382716411291943,0.));
#31940=DIRECTION('center_axis',(0.,0.,-1.));
#31941=DIRECTION('ref_axis',(-0.923865871502902,0.382716411291943,0.));
#31942=DIRECTION('center_axis',(0.707132021900493,0.707081539571584,0.));
#31943=DIRECTION('ref_axis',(-0.499982151482891,0.500017847879993,0.707106781186548));
#31944=DIRECTION('center_axis',(-0.70713202190049,-0.707081539571586,0.));
#31945=DIRECTION('ref_axis',(0.,0.,1.));
#31946=DIRECTION('',(-0.707132021900493,-0.707081539571584,0.));
#31947=DIRECTION('',(0.707132021900493,0.707081539571584,0.));
#31948=DIRECTION('center_axis',(0.,0.,-1.));
#31949=DIRECTION('ref_axis',(-1.,0.,0.));
#31950=DIRECTION('center_axis',(-0.999999999362884,3.56963971004377E-5,
0.));
#31951=DIRECTION('ref_axis',(0.,0.,1.));
#31952=DIRECTION('center_axis',(0.,0.,1.));
#31953=DIRECTION('ref_axis',(-0.382650452950611,0.923893192342433,0.));
#31954=DIRECTION('center_axis',(0.,0.,-1.));
#31955=DIRECTION('ref_axis',(-0.382650452950611,0.923893192342433,0.));
#31956=DIRECTION('center_axis',(0.999999999362884,-3.56963971021026E-5,
0.));
#31957=DIRECTION('ref_axis',(2.52411644548245E-5,0.707106780736035,0.707106781186551));
#31958=DIRECTION('center_axis',(-0.999999999362884,3.5696397104879E-5,0.));
#31959=DIRECTION('ref_axis',(0.,0.,1.));
#31960=DIRECTION('',(-0.999999999362884,3.56963971021026E-5,0.));
#31961=DIRECTION('',(0.999999999362884,-3.56963971021026E-5,0.));
#31962=DIRECTION('center_axis',(0.,0.,-1.));
#31963=DIRECTION('ref_axis',(-1.,0.,0.));
#31964=DIRECTION('center_axis',(-3.56963971004376E-5,-0.999999999362884,
0.));
#31965=DIRECTION('ref_axis',(0.,0.,1.));
#31966=DIRECTION('center_axis',(0.,0.,-1.));
#31967=DIRECTION('ref_axis',(0.707081539571587,-0.70713202190049,0.));
#31968=DIRECTION('center_axis',(0.,0.,1.));
#31969=DIRECTION('ref_axis',(0.707081539571586,-0.70713202190049,0.));
#31970=DIRECTION('center_axis',(3.56963971011028E-5,0.999999999362884,0.));
#31971=DIRECTION('ref_axis',(-0.707106780736038,2.52411644541176E-5,0.707106781186548));
#31972=DIRECTION('center_axis',(-3.56963970915558E-5,-0.999999999362884,
0.));
#31973=DIRECTION('ref_axis',(0.,0.,1.));
#31974=DIRECTION('',(-3.56963971011028E-5,-0.999999999362884,0.));
#31975=DIRECTION('',(3.56963971011028E-5,0.999999999362884,0.));
#31976=DIRECTION('center_axis',(1.,0.,0.));
#31977=DIRECTION('ref_axis',(0.,0.707106781186554,0.707106781186541));
#31978=DIRECTION('center_axis',(1.,0.,0.));
#31979=DIRECTION('ref_axis',(0.,1.,0.));
#31980=DIRECTION('',(1.,0.,0.));
#31981=DIRECTION('center_axis',(-1.,0.,0.));
#31982=DIRECTION('ref_axis',(0.,0.,1.));
#31983=DIRECTION('',(-1.,0.,0.));
#31984=DIRECTION('center_axis',(-0.999999999840721,1.78481985534681E-5,
0.));
#31985=DIRECTION('ref_axis',(1.26205822291212E-5,0.707106781073918,0.70710678118655));
#31986=DIRECTION('',(-0.999999999840721,1.78481985534681E-5,0.));
#31987=DIRECTION('center_axis',(0.999999999840721,-1.78481985546596E-5,
0.));
#31988=DIRECTION('ref_axis',(1.78481985546596E-5,0.999999999840721,0.));
#31989=DIRECTION('',(0.999999999840721,-1.78481985534681E-5,0.));
#31990=DIRECTION('center_axis',(0.999999999362884,-3.56963971040562E-5,
0.));
#31991=DIRECTION('ref_axis',(2.52411644562058E-5,0.707106780736035,0.707106781186551));
#31992=DIRECTION('',(-0.999999999362884,3.56963971040562E-5,0.));
#31993=DIRECTION('center_axis',(0.999999999362884,-3.5696397104879E-5,0.));
#31994=DIRECTION('ref_axis',(3.5696397104879E-5,0.999999999362884,0.));
#31995=DIRECTION('',(0.999999999362884,-3.56963971040562E-5,0.));
#31996=DIRECTION('center_axis',(-0.816511153790762,-0.408241003122002,-0.408226431169298));
#31997=DIRECTION('ref_axis',(-0.577329659497308,0.577370878146268,0.577350269189622));
#31998=DIRECTION('center_axis',(0.,0.,1.));
#31999=DIRECTION('ref_axis',(-0.999999999362884,3.56963970915558E-5,0.));
#32000=DIRECTION('center_axis',(0.408248290463868,-0.816496580927721,0.408248290463868));
#32001=DIRECTION('ref_axis',(0.577350269189616,0.577350269189634,0.577350269189627));
#32002=DIRECTION('center_axis',(0.,0.,1.));
#32003=DIRECTION('ref_axis',(-4.44089209850064E-15,1.,0.));
#32004=DIRECTION('center_axis',(0.469440044438886,-0.882964350739721,0.));
#32005=DIRECTION('ref_axis',(-0.882964350739721,-0.469440044438886,0.));
#32006=DIRECTION('',(0.,0.,-1.));
#32007=DIRECTION('',(-0.882964350739721,-0.469440044438886,0.));
#32008=DIRECTION('',(0.,0.,-1.));
#32009=DIRECTION('center_axis',(0.,0.,-1.));
#32010=DIRECTION('ref_axis',(-0.999999999362884,3.56963971004376E-5,0.));
#32011=DIRECTION('',(0.,0.,-1.));
#32012=DIRECTION('center_axis',(0.,0.,1.));
#32013=DIRECTION('ref_axis',(-0.857148915152355,0.51506867236626,0.));
#32014=DIRECTION('center_axis',(0.999999999362884,-3.56963971014961E-5,
0.));
#32015=DIRECTION('ref_axis',(-3.56963971014961E-5,-0.999999999362884,0.));
#32016=DIRECTION('',(0.,0.,-1.));
#32017=DIRECTION('',(-3.56963971014961E-5,-0.999999999362884,0.));
#32018=DIRECTION('center_axis',(0.707081539571584,-0.707132021900493,0.));
#32019=DIRECTION('ref_axis',(-0.707132021900493,-0.707081539571584,0.));
#32020=DIRECTION('',(0.,0.,-1.));
#32021=DIRECTION('',(-0.707132021900493,-0.707081539571584,0.));
#32022=DIRECTION('center_axis',(-3.5696397100931E-5,-0.999999999362884,
0.));
#32023=DIRECTION('ref_axis',(-0.999999999362884,3.5696397100931E-5,0.));
#32024=DIRECTION('',(0.,0.,-1.));
#32025=DIRECTION('',(-0.999999999362884,3.5696397100931E-5,0.));
#32026=DIRECTION('center_axis',(0.,0.,-1.));
#32027=DIRECTION('ref_axis',(-3.56963971004376E-5,-0.999999999362884,0.));
#32028=DIRECTION('',(0.,0.,-1.));
#32029=DIRECTION('center_axis',(0.,0.,-1.));
#32030=DIRECTION('ref_axis',(-0.707132021900492,-0.707081539571584,0.));
#32031=DIRECTION('center_axis',(-0.999999999362884,3.56963971007665E-5,
0.));
#32032=DIRECTION('ref_axis',(3.56963971007665E-5,0.999999999362884,0.));
#32033=DIRECTION('',(0.,0.,-1.));
#32034=DIRECTION('',(3.56963971007665E-5,0.999999999362884,0.));
#32035=DIRECTION('center_axis',(0.,0.,-1.));
#32036=DIRECTION('ref_axis',(-0.999999999362884,3.56963971013258E-5,0.));
#32037=DIRECTION('',(0.,0.,-1.));
#32038=DIRECTION('center_axis',(0.,0.,-1.));
#32039=DIRECTION('ref_axis',(-0.923865871502902,0.382716411291943,0.));
#32040=DIRECTION('center_axis',(-0.707081539571584,0.707132021900493,0.));
#32041=DIRECTION('ref_axis',(0.707132021900493,0.707081539571584,0.));
#32042=DIRECTION('',(0.,0.,-1.));
#32043=DIRECTION('',(0.707132021900493,0.707081539571584,0.));
#32044=DIRECTION('center_axis',(0.,0.,-1.));
#32045=DIRECTION('ref_axis',(-0.707081539571585,0.707132021900492,0.));
#32046=DIRECTION('',(0.,0.,-1.));
#32047=DIRECTION('center_axis',(0.,0.,1.));
#32048=DIRECTION('ref_axis',(-0.707081539571585,0.707132021900492,0.));
#32049=DIRECTION('',(0.,0.,-1.));
#32050=DIRECTION('center_axis',(0.,0.,-1.));
#32051=DIRECTION('ref_axis',(-0.674257203707391,0.738496596639883,0.));
#32052=DIRECTION('center_axis',(3.56963971021026E-5,0.999999999362884,0.));
#32053=DIRECTION('ref_axis',(0.999999999362884,-3.56963971021026E-5,0.));
#32054=DIRECTION('',(0.,0.,-1.));
#32055=DIRECTION('',(-0.999999999362884,3.56963971021026E-5,0.));
#32056=DIRECTION('center_axis',(0.,0.,-1.));
#32057=DIRECTION('ref_axis',(0.999999999362884,-3.56963970980596E-5,0.));
#32058=DIRECTION('',(0.,0.,-1.));
#32059=DIRECTION('center_axis',(0.,0.,-1.));
#32060=DIRECTION('ref_axis',(0.999999999362884,-3.56963970980596E-5,0.));
#32061=DIRECTION('center_axis',(-0.999999999362884,3.56963971011028E-5,
0.));
#32062=DIRECTION('ref_axis',(3.56963971011028E-5,0.999999999362884,0.));
#32063=DIRECTION('',(0.,0.,-1.));
#32064=DIRECTION('',(3.56963971011028E-5,0.999999999362884,0.));
#32065=DIRECTION('',(0.,0.,1.));
#32066=DIRECTION('',(-3.56963971011028E-5,-0.999999999362884,0.));
#32067=DIRECTION('center_axis',(0.,0.,-1.));
#32068=DIRECTION('ref_axis',(-0.999999999362884,3.56963970915558E-5,0.));
#32069=DIRECTION('',(0.,0.,-1.));
#32070=DIRECTION('center_axis',(0.,0.,-1.));
#32071=DIRECTION('ref_axis',(-0.999999999362884,3.56963970915558E-5,0.));
#32072=DIRECTION('center_axis',(3.56963971040562E-5,0.999999999362884,0.));
#32073=DIRECTION('ref_axis',(0.999999999362884,-3.56963971040562E-5,0.));
#32074=DIRECTION('',(0.,0.,-1.));
#32075=DIRECTION('',(0.999999999362884,-3.56963971040562E-5,0.));
#32076=DIRECTION('center_axis',(1.78481985534681E-5,0.999999999840721,0.));
#32077=DIRECTION('ref_axis',(0.999999999840721,-1.78481985534681E-5,0.));
#32078=DIRECTION('',(0.,0.,-1.));
#32079=DIRECTION('',(0.999999999840721,-1.78481985534681E-5,0.));
#32080=DIRECTION('center_axis',(0.,1.,0.));
#32081=DIRECTION('ref_axis',(1.,0.,0.));
#32082=DIRECTION('',(0.,0.,-1.));
#32083=DIRECTION('',(1.,0.,0.));
#32084=DIRECTION('center_axis',(0.,0.,-1.));
#32085=DIRECTION('ref_axis',(-1.,0.,0.));
#32086=DIRECTION('center_axis',(3.56963971011028E-5,0.999999999362884,0.));
#32087=DIRECTION('ref_axis',(-0.707106780736038,2.52411644541176E-5,-0.707106781186548));
#32088=DIRECTION('center_axis',(-3.56963970915558E-5,-0.999999999362884,
0.));
#32089=DIRECTION('ref_axis',(-0.999999999362884,3.56963970915558E-5,0.));
#32090=DIRECTION('',(-3.56963971011028E-5,-0.999999999362884,0.));
#32091=DIRECTION('center_axis',(0.,0.,1.));
#32092=DIRECTION('ref_axis',(1.,0.,0.));
#32093=DIRECTION('center_axis',(0.,0.,-1.));
#32094=DIRECTION('ref_axis',(0.880581945986775,-0.473893908382608,0.));
#32095=DIRECTION('center_axis',(0.,0.,1.));
#32096=DIRECTION('ref_axis',(0.880581945986775,-0.473893908382608,0.));
#32097=DIRECTION('center_axis',(0.999999999362884,-3.56963971040562E-5,
0.));
#32098=DIRECTION('ref_axis',(2.52411644562058E-5,0.707106780736035,-0.707106781186551));
#32099=DIRECTION('center_axis',(-0.999999999362884,3.56963971004374E-5,
0.));
#32100=DIRECTION('ref_axis',(3.56963971004374E-5,0.999999999362884,0.));
#32101=DIRECTION('',(-0.999999999362884,3.56963971040562E-5,0.));
#32102=DIRECTION('center_axis',(0.999999999362884,-3.56963971048783E-5,
0.));
#32103=DIRECTION('ref_axis',(0.,0.,-1.));
#32104=DIRECTION('center_axis',(0.999999999840721,-1.78481985534681E-5,
0.));
#32105=DIRECTION('ref_axis',(1.26205822291212E-5,0.707106781073918,-0.70710678118655));
#32106=DIRECTION('center_axis',(-0.999999999840721,1.78481985457778E-5,
0.));
#32107=DIRECTION('ref_axis',(1.78481985457778E-5,0.999999999840721,0.));
#32108=DIRECTION('',(-0.999999999840721,1.78481985534681E-5,0.));
#32109=DIRECTION('center_axis',(1.,0.,0.));
#32110=DIRECTION('ref_axis',(0.,0.707106781186554,-0.707106781186541));
#32111=DIRECTION('center_axis',(-1.,0.,0.));
#32112=DIRECTION('ref_axis',(0.,1.,0.));
#32113=DIRECTION('',(-1.,0.,0.));
#32114=DIRECTION('center_axis',(-0.816511153790763,-0.408241003122,0.408226431169296));
#32115=DIRECTION('ref_axis',(-0.57732965949731,0.577370878146255,-0.577350269189634));
#32116=DIRECTION('center_axis',(0.,0.,1.));
#32117=DIRECTION('ref_axis',(-0.836963911810301,-0.547258083839059,0.));
#32118=DIRECTION('center_axis',(0.,0.,1.));
#32119=DIRECTION('ref_axis',(-0.880598861730879,-0.473862474477859,0.));
#32120=DIRECTION('center_axis',(0.,0.,-1.));
#32121=DIRECTION('ref_axis',(-0.88059886173088,-0.473862474477859,0.));
#32122=DIRECTION('center_axis',(0.,-1.,0.));
#32123=DIRECTION('ref_axis',(0.707106781186548,0.,-0.707106781186548));
#32124=DIRECTION('',(0.,1.,0.));
#32125=DIRECTION('center_axis',(0.,-1.,0.));
#32126=DIRECTION('ref_axis',(0.,0.,-1.));
#32127=DIRECTION('',(0.,-1.,0.));
#32128=DIRECTION('center_axis',(0.408248290463864,-0.816496580927721,-0.408248290463871));
#32129=DIRECTION('ref_axis',(0.577350269189621,0.577350269189625,-0.577350269189632));
#32130=DIRECTION('center_axis',(0.,0.,-1.));
#32131=DIRECTION('ref_axis',(-4.44089209850064E-15,1.,0.));
#32132=DIRECTION('center_axis',(0.707132021900493,0.707081539571584,0.));
#32133=DIRECTION('ref_axis',(-0.499982151482891,0.500017847879993,-0.707106781186548));
#32134=DIRECTION('',(-0.707132021900493,-0.707081539571584,0.));
#32135=DIRECTION('center_axis',(-0.707132021900495,-0.707081539571582,0.));
#32136=DIRECTION('ref_axis',(-0.707081539571582,0.707132021900495,0.));
#32137=DIRECTION('center_axis',(-0.70713202190049,-0.707081539571586,0.));
#32138=DIRECTION('ref_axis',(-0.707081539571586,0.70713202190049,0.));
#32139=DIRECTION('center_axis',(0.,0.,-1.));
#32140=DIRECTION('ref_axis',(-1.,0.,0.));
#32141=DIRECTION('',(-0.707106781186548,0.707106781186547,0.));
#32142=DIRECTION('center_axis',(0.,0.,1.));
#32143=DIRECTION('ref_axis',(0.923879532511287,0.38268343236509,0.));
#32144=DIRECTION('',(3.28954970259306E-16,1.,0.));
#32145=DIRECTION('center_axis',(0.,0.,1.));
#32146=DIRECTION('ref_axis',(0.707106781186547,-0.707106781186548,0.));
#32147=DIRECTION('',(1.,0.,0.));
#32148=DIRECTION('',(0.707106781186548,-0.707106781186547,0.));
#32149=DIRECTION('',(0.,-1.,0.));
#32150=DIRECTION('center_axis',(0.,0.,-1.));
#32151=DIRECTION('ref_axis',(0.857167300702112,0.515038074910055,0.));
#32152=DIRECTION('',(0.882947592858928,-0.46947156278589,0.));
#32153=DIRECTION('',(1.,0.,0.));
#32154=DIRECTION('',(0.999999999840721,-1.7848198553344E-5,0.));
#32155=DIRECTION('',(0.999999999362884,-3.56963971010297E-5,0.));
#32156=DIRECTION('',(0.882964350739721,0.469440044438886,0.));
#32157=DIRECTION('center_axis',(0.,0.,-1.));
#32158=DIRECTION('ref_axis',(-0.857148915152355,0.51506867236626,0.));
#32159=DIRECTION('',(3.56963971014961E-5,0.999999999362884,0.));
#32160=DIRECTION('',(0.707132021900493,0.707081539571584,0.));
#32161=DIRECTION('',(0.999999999362884,-3.5696397100931E-5,0.));
#32162=DIRECTION('center_axis',(0.,0.,1.));
#32163=DIRECTION('ref_axis',(-0.707132021900492,-0.707081539571584,0.));
#32164=DIRECTION('',(-3.56963971007665E-5,-0.999999999362884,0.));
#32165=DIRECTION('center_axis',(0.,0.,1.));
#32166=DIRECTION('ref_axis',(-0.923865871502902,0.382716411291943,0.));
#32167=DIRECTION('center_axis',(0.707106781186548,-0.707106781186547,0.));
#32168=DIRECTION('ref_axis',(0.5,0.500000000000001,-0.707106781186547));
#32169=DIRECTION('center_axis',(-0.707106781186548,0.707106781186548,0.));
#32170=DIRECTION('ref_axis',(0.707106781186548,0.707106781186548,0.));
#32171=DIRECTION('',(0.707106781186548,-0.707106781186547,0.));
#32172=DIRECTION('center_axis',(-0.707106781186548,0.707106781186548,0.));
#32173=DIRECTION('ref_axis',(0.707106781186548,0.707106781186548,0.));
#32174=DIRECTION('center_axis',(0.,0.,-1.));
#32175=DIRECTION('ref_axis',(-1.,0.,0.));
#32176=DIRECTION('center_axis',(0.,0.,-1.));
#32177=DIRECTION('ref_axis',(0.674283564945582,0.738472527616483,0.));
#32178=DIRECTION('center_axis',(-0.999999999362884,3.5696397100931E-5,0.));
#32179=DIRECTION('ref_axis',(-2.52411644539961E-5,-0.707106780736038,-0.707106781186548));
#32180=DIRECTION('center_axis',(0.999999999362884,-3.56963971004376E-5,
0.));
#32181=DIRECTION('ref_axis',(-3.56963971004376E-5,-0.999999999362884,0.));
#32182=DIRECTION('center_axis',(-0.923893192342434,-0.38265045295061,-1.69930937299605E-15));
#32183=DIRECTION('ref_axis',(0.38265045295061,-0.923893192342434,-4.10249573495478E-15));
#32184=DIRECTION('center_axis',(-3.56963971048783E-5,-0.999999999362884,
0.));
#32185=DIRECTION('ref_axis',(-0.999999999362884,3.56963971048783E-5,0.));
#32186=DIRECTION('center_axis',(3.56963971007665E-5,0.999999999362884,0.));
#32187=DIRECTION('ref_axis',(-0.707106780736035,2.52411644538797E-5,-0.707106781186551));
#32188=DIRECTION('center_axis',(-3.56963971004377E-5,-0.999999999362884,
0.));
#32189=DIRECTION('ref_axis',(-0.999999999362884,3.56963971004377E-5,0.));
#32190=DIRECTION('center_axis',(0.,0.,-1.));
#32191=DIRECTION('ref_axis',(-1.,0.,0.));
#32192=DIRECTION('center_axis',(0.,0.,-1.));
#32193=DIRECTION('ref_axis',(-1.,0.,0.));
#32194=DIRECTION('center_axis',(-0.707132021900493,-0.707081539571584,0.));
#32195=DIRECTION('ref_axis',(0.499982151482891,-0.500017847879993,-0.707106781186548));
#32196=DIRECTION('center_axis',(-0.382716411291948,-0.9238658715029,-4.10278864883162E-15));
#32197=DIRECTION('ref_axis',(0.9238658715029,-0.382716411291948,-9.90500799955984E-15));
#32198=DIRECTION('center_axis',(-0.882964350739721,-0.469440044438886,0.));
#32199=DIRECTION('ref_axis',(0.33194423878325,-0.624350079954033,-0.707106781186549));
#32200=DIRECTION('center_axis',(0.88296435073972,0.469440044438887,0.));
#32201=DIRECTION('ref_axis',(0.469440044438887,-0.88296435073972,0.));
#32202=DIRECTION('center_axis',(-0.970304361397861,-0.241887259383973,0.));
#32203=DIRECTION('ref_axis',(-0.241887259383973,0.970304361397861,0.));
#32204=DIRECTION('center_axis',(0.,0.,1.));
#32205=DIRECTION('ref_axis',(1.,0.,0.));
#32206=DIRECTION('center_axis',(3.56963971004376E-5,0.999999999362884,0.));
#32207=DIRECTION('ref_axis',(0.999999999362884,-3.56963971004376E-5,0.));
#32208=DIRECTION('center_axis',(-3.56963971014961E-5,-0.999999999362884,
0.));
#32209=DIRECTION('ref_axis',(0.707106780736038,-2.52411644543957E-5,-0.707106781186548));
#32210=DIRECTION('center_axis',(-1.,0.,0.));
#32211=DIRECTION('ref_axis',(0.,-0.707106781186548,-0.707106781186548));
#32212=DIRECTION('',(-1.,0.,0.));
#32213=DIRECTION('center_axis',(1.,0.,0.));
#32214=DIRECTION('ref_axis',(0.,-1.,0.));
#32215=DIRECTION('center_axis',(-0.970295726275993,0.241921895599681,0.));
#32216=DIRECTION('ref_axis',(0.241921895599681,0.970295726275993,0.));
#32217=DIRECTION('center_axis',(-0.999999999840721,1.7848198553344E-5,0.));
#32218=DIRECTION('ref_axis',(-1.26205822290334E-5,-0.707106781073918,-0.70710678118655));
#32219=DIRECTION('center_axis',(0.999999999840721,-1.78481985502188E-5,
0.));
#32220=DIRECTION('ref_axis',(-1.78481985502188E-5,-0.999999999840721,0.));
#32221=DIRECTION('',(-0.999999999840721,1.7848198553344E-5,0.));
#32222=DIRECTION('center_axis',(-0.999999999362884,3.56963971010297E-5,
0.));
#32223=DIRECTION('ref_axis',(-2.52411644540658E-5,-0.707106780736035,-0.707106781186551));
#32224=DIRECTION('',(-0.999999999362884,3.56963971010297E-5,0.));
#32225=DIRECTION('center_axis',(0.,1.,0.));
#32226=DIRECTION('ref_axis',(-0.707106781186551,0.,-0.707106781186544));
#32227=DIRECTION('',(0.,1.,0.));
#32228=DIRECTION('center_axis',(0.,-1.,0.));
#32229=DIRECTION('ref_axis',(-1.,0.,0.));
#32230=DIRECTION('center_axis',(-0.382683432365083,0.92387953251129,0.));
#32231=DIRECTION('ref_axis',(-0.92387953251129,-0.382683432365083,0.));
#32232=DIRECTION('center_axis',(0.,0.,1.));
#32233=DIRECTION('ref_axis',(1.,0.,0.));
#32234=DIRECTION('center_axis',(0.88294759285893,-0.469471562785885,0.));
#32235=DIRECTION('ref_axis',(-0.469471562785885,-0.88294759285893,0.));
#32236=DIRECTION('center_axis',(0.,0.,1.));
#32237=DIRECTION('ref_axis',(0.857167300702112,0.515038074910055,0.));
#32238=DIRECTION('center_axis',(-0.882947592858928,0.46947156278589,0.));
#32239=DIRECTION('ref_axis',(-0.331966525620151,-0.624338230342891,-0.707106781186542));
#32240=DIRECTION('',(-0.882947592858928,0.46947156278589,0.));
#32241=DIRECTION('center_axis',(-0.707106781186548,0.707106781186547,0.));
#32242=DIRECTION('ref_axis',(-0.5,-0.500000000000001,-0.707106781186547));
#32243=DIRECTION('',(-0.707106781186548,0.707106781186547,0.));
#32244=DIRECTION('center_axis',(-0.92387953251129,0.382683432365083,0.));
#32245=DIRECTION('ref_axis',(-0.382683432365083,-0.92387953251129,0.));
#32246=DIRECTION('center_axis',(0.,0.,-1.));
#32247=DIRECTION('ref_axis',(-1.,0.,0.));
#32248=DIRECTION('center_axis',(0.,1.,0.));
#32249=DIRECTION('ref_axis',(1.,0.,0.));
#32250=DIRECTION('center_axis',(0.,0.,-1.));
#32251=DIRECTION('ref_axis',(0.923879532511287,0.38268343236509,0.));
#32252=DIRECTION('center_axis',(-3.28954970259306E-16,-1.,0.));
#32253=DIRECTION('ref_axis',(0.707106781186548,-2.32606290175374E-16,-0.707106781186548));
#32254=DIRECTION('center_axis',(0.,1.,0.));
#32255=DIRECTION('ref_axis',(1.,0.,0.));
#32256=DIRECTION('',(-3.28954970259306E-16,-1.,0.));
#32257=DIRECTION('center_axis',(1.,0.,0.));
#32258=DIRECTION('ref_axis',(0.,-1.,0.));
#32259=DIRECTION('center_axis',(0.,0.,-1.));
#32260=DIRECTION('ref_axis',(0.707106781186546,-0.707106781186549,0.));
#32261=DIRECTION('center_axis',(-1.,0.,0.));
#32262=DIRECTION('ref_axis',(0.,-0.707106781186548,-0.707106781186548));
#32263=DIRECTION('',(-1.,0.,0.));
#32264=DIRECTION('center_axis',(-3.56963971010297E-5,-0.999999999362884,
0.));
#32265=DIRECTION('ref_axis',(-0.999999999362884,3.56963971010297E-5,0.));
#32266=DIRECTION('',(0.,0.,-1.));
#32267=DIRECTION('center_axis',(-1.7848198553344E-5,-0.999999999840721,
0.));
#32268=DIRECTION('ref_axis',(-0.999999999840721,1.7848198553344E-5,0.));
#32269=DIRECTION('',(0.,0.,-1.));
#32270=DIRECTION('center_axis',(0.,-1.,0.));
#32271=DIRECTION('ref_axis',(-1.,0.,0.));
#32272=DIRECTION('',(0.,0.,-1.));
#32273=DIRECTION('center_axis',(-0.46947156278589,-0.882947592858928,0.));
#32274=DIRECTION('ref_axis',(-0.882947592858928,0.46947156278589,0.));
#32275=DIRECTION('',(0.,0.,-1.));
#32276=DIRECTION('center_axis',(0.,0.,-1.));
#32277=DIRECTION('ref_axis',(0.469471562785885,0.88294759285893,0.));
#32278=DIRECTION('',(0.,0.,-1.));
#32279=DIRECTION('center_axis',(-1.,0.,0.));
#32280=DIRECTION('ref_axis',(0.,1.,0.));
#32281=DIRECTION('',(0.,0.,-1.));
#32282=DIRECTION('center_axis',(-0.707106781186547,-0.707106781186548,0.));
#32283=DIRECTION('ref_axis',(-0.707106781186548,0.707106781186547,0.));
#32284=DIRECTION('',(0.,0.,-1.));
#32285=DIRECTION('center_axis',(0.,-1.,0.));
#32286=DIRECTION('ref_axis',(-1.,0.,0.));
#32287=DIRECTION('',(0.,0.,-1.));
#32288=DIRECTION('center_axis',(0.,0.,-1.));
#32289=DIRECTION('ref_axis',(1.,0.,0.));
#32290=DIRECTION('',(0.,0.,-1.));
#32291=DIRECTION('center_axis',(1.,-3.28954970259306E-16,0.));
#32292=DIRECTION('ref_axis',(-3.28954970259306E-16,-1.,0.));
#32293=DIRECTION('',(0.,0.,-1.));
#32294=DIRECTION('center_axis',(0.,0.,-1.));
#32295=DIRECTION('ref_axis',(0.707106781186547,0.707106781186548,0.));
#32296=DIRECTION('',(0.,0.,-1.));
#32297=DIRECTION('center_axis',(0.707106781186547,0.707106781186548,0.));
#32298=DIRECTION('ref_axis',(0.707106781186548,-0.707106781186547,0.));
#32299=DIRECTION('',(0.,0.,-1.));
#32300=DIRECTION('center_axis',(0.,0.,-1.));
#32301=DIRECTION('ref_axis',(1.48029736616687E-15,1.,0.));
#32302=DIRECTION('',(0.,0.,1.));
#32303=DIRECTION('center_axis',(0.,0.,1.));
#32304=DIRECTION('ref_axis',(1.48029736616687E-15,1.,0.));
#32305=DIRECTION('',(0.,0.,-1.));
#32306=DIRECTION('center_axis',(0.,0.,1.));
#32307=DIRECTION('ref_axis',(-1.,0.,0.));
#32308=DIRECTION('',(0.,0.,-1.));
#32309=DIRECTION('center_axis',(0.,0.,1.));
#32310=DIRECTION('ref_axis',(-1.,0.,0.));
#32311=DIRECTION('center_axis',(0.,0.,1.));
#32312=DIRECTION('ref_axis',(0.836944376135179,-0.547287960086548,0.));
#32313=DIRECTION('center_axis',(0.,0.,1.));
#32314=DIRECTION('ref_axis',(-1.,0.,0.));
#32315=DIRECTION('center_axis',(0.,0.,-1.));
#32316=DIRECTION('ref_axis',(-1.,0.,0.));
#32317=DIRECTION('center_axis',(0.,0.,-1.));
#32318=DIRECTION('ref_axis',(-1.,0.,0.));
#32319=DIRECTION('',(-1.,0.,0.));
#32320=DIRECTION('',(0.,1.,0.));
#32321=DIRECTION('center_axis',(0.,0.,-1.));
#32322=DIRECTION('ref_axis',(0.,-1.,0.));
#32323=DIRECTION('center_axis',(0.,1.,0.));
#32324=DIRECTION('ref_axis',(1.,0.,0.));
#32325=DIRECTION('',(0.,0.,-1.));
#32326=DIRECTION('center_axis',(0.,0.,-1.));
#32327=DIRECTION('ref_axis',(0.,-1.,0.));
#32328=DIRECTION('',(0.,0.,-1.));
#32329=DIRECTION('center_axis',(1.,0.,0.));
#32330=DIRECTION('ref_axis',(0.,-1.,0.));
#32331=DIRECTION('',(0.,0.,-1.));
#32332=DIRECTION('center_axis',(0.,0.,-1.));
#32333=DIRECTION('ref_axis',(-4.44089209850064E-15,1.,0.));
#124428=CARTESIAN_POINT('',(0.,0.,0.));
#124429=CARTESIAN_POINT('Origin',(25.9997814655409,18.8808065108639,21.5));
#124430=CARTESIAN_POINT('',(22.9997814655409,18.8808065108619,18.5));
#124431=CARTESIAN_POINT('Origin',(22.9997814655409,18.8808065108619,21.5));
#124432=CARTESIAN_POINT('',(25.9997805061207,18.8808065108639,18.5));
#124433=CARTESIAN_POINT('',(25.9997814655409,18.8808065108639,18.5));
#124434=CARTESIAN_POINT('Origin',(25.9997805061207,18.8808065108639,21.5));
#124435=CARTESIAN_POINT('Origin',(22.9997814655409,18.8808065108619,21.5));
#124436=CARTESIAN_POINT('Origin',(-26.0001963416363,18.8817346167756,21.5));
#124437=CARTESIAN_POINT('',(-26.0001963416363,18.8817346167756,18.5));
#124438=CARTESIAN_POINT('Origin',(-26.0001963416363,18.8817346167756,21.5));
#124439=CARTESIAN_POINT('',(-23.0001963435476,18.8816275275843,18.5));
#124440=CARTESIAN_POINT('',(-26.0001963416363,18.8817346167756,18.5));
#124441=CARTESIAN_POINT('Origin',(-23.0001963435476,18.8816275275843,21.5));
#124442=CARTESIAN_POINT('Origin',(-23.0001963435476,18.8816275275843,21.5));
#124443=CARTESIAN_POINT('Origin',(-6.00033197323811,24.630714186474,25.5));
#124444=CARTESIAN_POINT('',(-15.7502284469069,24.1310622223319,25.5));
#124445=CARTESIAN_POINT('',(-12.0002284492961,24.1309283608428,25.5));
#124446=CARTESIAN_POINT('',(-6.00034982143666,24.1307141867926,25.5));
#124447=CARTESIAN_POINT('',(-12.0002106010975,24.6309283605242,26.));
#124448=CARTESIAN_POINT('Origin',(-12.0002106010975,24.6309283605242,25.5));
#124449=CARTESIAN_POINT('',(-15.8748746000505,24.631066672069,26.));
#124450=CARTESIAN_POINT('',(-6.00033197323811,24.630714186474,26.));
#124451=CARTESIAN_POINT('Origin',(-15.8748746000505,24.631066672069,25.5));
#124452=CARTESIAN_POINT('Origin',(5.99980902926158,24.6306070926795,25.5));
#124453=CARTESIAN_POINT('',(12.,24.1305,25.5));
#124454=CARTESIAN_POINT('',(5.9998001051623,24.1306070927591,25.5));
#124455=CARTESIAN_POINT('',(12.0000089240993,24.6304999999204,26.));
#124456=CARTESIAN_POINT('Origin',(12.0000089240993,24.6304999999204,25.5));
#124457=CARTESIAN_POINT('',(5.99980902926158,24.6306070926795,26.));
#124458=CARTESIAN_POINT('Origin',(15.5005576038968,36.3806823573572,25.5));
#124459=CARTESIAN_POINT('',(16.0005576038968,44.6304565378295,25.5));
#124460=CARTESIAN_POINT('',(15.5005576038968,44.6304565378295,26.));
#124461=CARTESIAN_POINT('Origin',(15.5005576038968,44.6304565378295,25.5));
#124462=CARTESIAN_POINT('',(15.5005576038968,36.1384565378295,26.));
#124463=CARTESIAN_POINT('',(15.5005576038968,36.3806823573572,26.));
#124464=CARTESIAN_POINT('',(16.0005576038968,36.1384565378295,25.5));
#124465=CARTESIAN_POINT('Origin',(15.5005576038968,36.1384565378295,25.5));
#124466=CARTESIAN_POINT('',(16.0005576038968,36.3806823573572,25.5));
#124467=CARTESIAN_POINT('Origin',(16.5085576038968,36.1384565378295,25.5));
#124468=CARTESIAN_POINT('',(16.5085576038968,35.1304565378295,26.));
#124469=CARTESIAN_POINT('',(16.5085576038968,35.6304565378295,25.5));
#124470=CARTESIAN_POINT('Origin',(16.5085576038968,35.1304565378295,25.5));
#124471=CARTESIAN_POINT('Origin',(16.5085576038968,36.1384565378295,25.5));
#124472=CARTESIAN_POINT('Origin',(16.5085576038968,36.1384565378295,26.));
#124473=CARTESIAN_POINT('Origin',(8.25411460523903,35.1304565378295,25.5));
#124474=CARTESIAN_POINT('',(16.8285576038968,35.1304565378295,26.));
#124475=CARTESIAN_POINT('',(16.8285576038968,35.6304565378295,25.5));
#124476=CARTESIAN_POINT('Origin',(16.8285576038968,35.1304565378295,25.5));
#124477=CARTESIAN_POINT('',(8.25411460523903,35.6304565378295,25.5));
#124478=CARTESIAN_POINT('',(8.25411460523903,35.1304565378295,26.));
#124479=CARTESIAN_POINT('Origin',(16.8285576038968,32.6304565378295,25.5));
#124480=CARTESIAN_POINT('',(18.5963245568632,34.3982234907959,26.));
#124481=CARTESIAN_POINT('',(18.9498779474565,34.7517768813891,25.5));
#124482=CARTESIAN_POINT('Origin',(18.5963245568632,34.3982234907959,25.5));
#124483=CARTESIAN_POINT('Origin',(16.8285576038968,32.6304565378295,25.5));
#124484=CARTESIAN_POINT('Origin',(16.8285576038968,32.6304565378295,26.));
#124485=CARTESIAN_POINT('Origin',(15.5139901477705,37.4805578998886,25.5));
#124486=CARTESIAN_POINT('',(24.1817610214557,28.8127870262033,26.));
#124487=CARTESIAN_POINT('',(24.535314412049,29.1663404167966,25.5));
#124488=CARTESIAN_POINT('Origin',(24.1817610214557,28.8127870262033,25.5));
#124489=CARTESIAN_POINT('',(15.8675435383638,37.8341112904819,25.5));
#124490=CARTESIAN_POINT('',(15.5139901477705,37.4805578998886,26.));
#124491=CARTESIAN_POINT('Origin',(20.9997805061163,25.6308065108639,25.5));
#124492=CARTESIAN_POINT('',(25.4997805061163,25.6308065108639,26.));
#124493=CARTESIAN_POINT('',(25.9997805061163,25.6308065108639,25.5));
#124494=CARTESIAN_POINT('Origin',(25.4997805061163,25.6308065108639,25.5));
#124495=CARTESIAN_POINT('Origin',(20.9997805061163,25.6308065108639,25.5));
#124496=CARTESIAN_POINT('Origin',(20.9997805061163,25.6308065108639,26.));
#124497=CARTESIAN_POINT('Origin',(25.4997805061163,26.8808573438743,25.5));
#124498=CARTESIAN_POINT('',(25.4997805061163,12.1308065108639,26.));
#124499=CARTESIAN_POINT('',(25.9997805061163,12.1308065108639,25.5));
#124500=CARTESIAN_POINT('Origin',(25.4997805061163,12.1308065108639,25.5));
#124501=CARTESIAN_POINT('',(25.9997805061163,26.8808573438743,25.5));
#124502=CARTESIAN_POINT('',(25.4997805061163,26.8808573438743,26.));
#124503=CARTESIAN_POINT('Ctrl Pts',(25.4997805061163,12.1308065108638,26.));
#124504=CARTESIAN_POINT('Ctrl Pts',(25.4997805061163,11.6308065108639,26.));
#124505=CARTESIAN_POINT('Ctrl Pts',(24.9997805061164,11.630806510864,26.));
#124506=CARTESIAN_POINT('Ctrl Pts',(25.9997805061163,12.1308065108638,26.));
#124507=CARTESIAN_POINT('Ctrl Pts',(25.9997805061164,11.1308065108638,26.));
#124508=CARTESIAN_POINT('Ctrl Pts',(24.9997805061164,11.1308065108639,26.));
#124509=CARTESIAN_POINT('Ctrl Pts',(25.9997805061163,12.1308065108638,25.5));
#124510=CARTESIAN_POINT('Ctrl Pts',(25.9997805061164,11.1308065108638,25.5));
#124511=CARTESIAN_POINT('Ctrl Pts',(24.9997805061164,11.1308065108639,25.5));
#124512=CARTESIAN_POINT('',(24.9997805061163,11.6308065108639,26.));
#124513=CARTESIAN_POINT('',(24.9997805061163,11.1308065108639,25.5));
#124514=CARTESIAN_POINT('Origin',(24.9997805061163,11.6308065108639,25.5));
#124515=CARTESIAN_POINT('Origin',(24.9997805061163,12.1308065108639,25.5));
#124516=CARTESIAN_POINT('Origin',(24.9997805061163,12.1308065108639,26.));
#124517=CARTESIAN_POINT('Origin',(12.4997260563488,11.6308065108639,25.5));
#124518=CARTESIAN_POINT('',(20.4997805061163,11.1308065108639,25.5));
#124519=CARTESIAN_POINT('',(12.4997260563488,11.1308065108639,25.5));
#124520=CARTESIAN_POINT('',(20.7068872873028,11.6308065108639,26.));
#124521=CARTESIAN_POINT('',(12.4997260563488,11.6308065108639,26.));
#124522=CARTESIAN_POINT('Origin',(20.7068872873028,11.6308065108639,25.5));
#124523=CARTESIAN_POINT('Origin',(11.4782812553205,20.8594125428461,25.5));
#124524=CARTESIAN_POINT('',(19.0000070232196,12.6305799937605,25.5));
#124525=CARTESIAN_POINT('',(11.1247278647273,20.5058591522529,25.5));
#124526=CARTESIAN_POINT('',(19.5000070232196,12.8376867749471,26.));
#124527=CARTESIAN_POINT('',(11.4782812553205,20.8594125428461,26.));
#124528=CARTESIAN_POINT('Origin',(19.5000070232196,12.8376867749471,25.5));
#124529=CARTESIAN_POINT('Origin',(19.5000070232196,20.3807440853227,25.5));
#124530=CARTESIAN_POINT('',(19.5000070232196,21.8015799937605,26.));
#124531=CARTESIAN_POINT('',(19.5000070232196,20.3807440853227,26.));
#124532=CARTESIAN_POINT('',(19.0000070232196,21.8015799937605,25.5));
#124533=CARTESIAN_POINT('Origin',(19.5000070232196,21.8015799937605,25.5));
#124534=CARTESIAN_POINT('',(19.0000070232196,20.3807440853227,25.5));
#124535=CARTESIAN_POINT('Origin',(18.0000070232196,21.8015799937605,25.5));
#124536=CARTESIAN_POINT('',(18.7042143673984,23.1260013830489,26.));
#124537=CARTESIAN_POINT('',(18.4694785860055,22.6845275866195,25.5));
#124538=CARTESIAN_POINT('Origin',(18.7042143673984,23.1260013830489,25.5));
#124539=CARTESIAN_POINT('Origin',(18.0000070232196,21.8015799937605,25.5));
#124540=CARTESIAN_POINT('Origin',(18.0000070232196,21.8015799937605,26.));
#124541=CARTESIAN_POINT('Origin',(10.3759028387591,27.5542431726415,25.5));
#124542=CARTESIAN_POINT('',(15.75,24.1305,25.5));
#124543=CARTESIAN_POINT('',(10.1411670573662,27.112769376212,25.5));
#124544=CARTESIAN_POINT('',(15.8746640014216,24.6305,26.));
#124545=CARTESIAN_POINT('',(10.3759028387591,27.5542431726415,26.));
#124546=CARTESIAN_POINT('Origin',(15.8746640014216,24.6305,25.5));
#124547=CARTESIAN_POINT('Origin',(7.87483580329061,24.6305,25.5));
#124548=CARTESIAN_POINT('',(7.87483580329061,24.1305,25.5));
#124549=CARTESIAN_POINT('',(7.87483580329061,24.6305,26.));
#124550=CARTESIAN_POINT('Origin',(-9.01646660547503,28.2774328600768,25.5));
#124551=CARTESIAN_POINT('',(-18.7044786694047,23.12666906083,26.));
#124552=CARTESIAN_POINT('',(-9.01646660547503,28.2774328600768,26.));
#124553=CARTESIAN_POINT('',(-18.4697586471852,22.6851868854601,25.5));
#124554=CARTESIAN_POINT('Origin',(-18.7044786694047,23.12666906083,25.5));
#124555=CARTESIAN_POINT('',(-8.78174658325559,27.8359506847069,25.5));
#124556=CARTESIAN_POINT('Origin',(-18.0003186027463,21.8022225347204,25.5));
#124557=CARTESIAN_POINT('',(-19.5003186017906,21.8022760793161,26.));
#124558=CARTESIAN_POINT('',(-19.0003186021092,21.8022582311175,25.5));
#124559=CARTESIAN_POINT('Origin',(-19.5003186017906,21.8022760793161,25.5));
#124560=CARTESIAN_POINT('Origin',(-18.0003186027463,21.8022225347204,25.5));
#124561=CARTESIAN_POINT('Origin',(-18.0003186027463,21.8022225347204,26.));
#124562=CARTESIAN_POINT('Origin',(-19.5002056346847,24.9669401637651,25.5));
#124563=CARTESIAN_POINT('',(-19.000645973767,12.6312582369605,25.5));
#124564=CARTESIAN_POINT('',(-19.0002056350033,24.9669223155665,25.5));
#124565=CARTESIAN_POINT('',(-19.5006385804826,12.8383828662136,26.));
#124566=CARTESIAN_POINT('',(-19.5002056346847,24.9669401637651,26.));
#124567=CARTESIAN_POINT('Origin',(-19.5006385804826,12.8383828662136,25.5));
#124568=CARTESIAN_POINT('Origin',(-10.7288557519193,21.609539475044,25.5));
#124569=CARTESIAN_POINT('',(-20.707561925074,11.6315456841765,26.));
#124570=CARTESIAN_POINT('',(-10.7288557519193,21.609539475044,26.));
#124571=CARTESIAN_POINT('',(-20.500472992218,11.1315382915292,25.5));
#124572=CARTESIAN_POINT('Origin',(-20.707561925074,11.6315456841765,25.5));
#124573=CARTESIAN_POINT('',(-10.3753149821335,21.2559734640938,25.5));
#124574=CARTESIAN_POINT('Origin',(-10.2506862658096,11.6311724113903,25.5));
#124575=CARTESIAN_POINT('',(-25.0004551411524,11.6316989249976,26.));
#124576=CARTESIAN_POINT('',(-10.2506862658096,11.6311724113903,26.));
#124577=CARTESIAN_POINT('',(-25.0004729893509,11.1316989253161,25.5));
#124578=CARTESIAN_POINT('Origin',(-25.0004551411524,11.6316989249976,25.5));
#124579=CARTESIAN_POINT('',(-10.2507041140081,11.1311724117089,25.5));
#124580=CARTESIAN_POINT('Ctrl Pts',(-25.0004551411524,11.6316989249976,
26.));
#124581=CARTESIAN_POINT('Ctrl Pts',(-25.5004551408338,11.6317167731961,
26.));
#124582=CARTESIAN_POINT('Ctrl Pts',(-25.5004372926352,12.1317167728775,
26.));
#124583=CARTESIAN_POINT('Ctrl Pts',(-25.0004729893508,11.1316989253161,
26.));
#124584=CARTESIAN_POINT('Ctrl Pts',(-26.000472988714,11.131734621713,26.0000000000001));
#124585=CARTESIAN_POINT('Ctrl Pts',(-26.0004372923167,12.1317346210762,
26.));
#124586=CARTESIAN_POINT('Ctrl Pts',(-25.0004729893509,11.1316989253161,
25.5));
#124587=CARTESIAN_POINT('Ctrl Pts',(-26.000472988714,11.131734621713,25.5));
#124588=CARTESIAN_POINT('Ctrl Pts',(-26.0004372923167,12.1317346210762,
25.5));
#124589=CARTESIAN_POINT('',(-25.5004372926353,12.1317167728775,26.));
#124590=CARTESIAN_POINT('',(-26.0004372923167,12.1317346210761,25.5));
#124591=CARTESIAN_POINT('Origin',(-25.5004372926353,12.1317167728775,25.5));
#124592=CARTESIAN_POINT('Origin',(-25.0004372929538,12.131698924679,25.5));
#124593=CARTESIAN_POINT('Origin',(-25.0004372929538,12.131698924679,26.));
#124594=CARTESIAN_POINT('Origin',(-25.5001517196441,20.1317675956942,25.5));
#124595=CARTESIAN_POINT('',(-25.4999553912744,25.6317167642765,26.));
#124596=CARTESIAN_POINT('',(-25.9999553909559,25.631734612475,25.5));
#124597=CARTESIAN_POINT('Origin',(-25.4999553912744,25.6317167642765,25.5));
#124598=CARTESIAN_POINT('',(-26.0001517193255,20.1317854438928,25.5));
#124599=CARTESIAN_POINT('',(-25.5001517196441,20.1317675956942,26.));
#124600=CARTESIAN_POINT('Origin',(-20.9999553941414,25.6315561304895,25.5));
#124601=CARTESIAN_POINT('',(-24.1818223222136,28.8136502290417,26.));
#124602=CARTESIAN_POINT('',(-24.5353630919994,29.167216239992,25.5));
#124603=CARTESIAN_POINT('Origin',(-24.1818223222136,28.8136502290417,25.5));
#124604=CARTESIAN_POINT('Origin',(-20.9999553941414,25.6315561304895,25.5));
#124605=CARTESIAN_POINT('Origin',(-20.9999553941414,25.6315561304895,26.));
#124606=CARTESIAN_POINT('Origin',(-18.3067027565145,34.6883503685105,25.5));
#124607=CARTESIAN_POINT('',(-18.5961864812216,34.3988873101177,26.));
#124608=CARTESIAN_POINT('',(-18.9497272510074,34.7524533210679,25.5));
#124609=CARTESIAN_POINT('Origin',(-18.5961864812216,34.3988873101177,25.5));
#124610=CARTESIAN_POINT('',(-18.6602435263003,35.0419163794607,25.5));
#124611=CARTESIAN_POINT('',(-18.3067027565145,34.6883503685105,26.));
#124612=CARTESIAN_POINT('Origin',(-16.8284826322926,32.6310572553665,25.5));
#124613=CARTESIAN_POINT('',(-16.8283933912999,35.1310572537737,26.));
#124614=CARTESIAN_POINT('',(-16.8283755431013,35.6310572534551,25.5));
#124615=CARTESIAN_POINT('Origin',(-16.8283933912999,35.1310572537737,25.5));
#124616=CARTESIAN_POINT('Origin',(-16.8284826322926,32.6310572553665,25.5));
#124617=CARTESIAN_POINT('Origin',(-16.8284826322926,32.6310572553665,26.));
#124618=CARTESIAN_POINT('Origin',(-8.41423596303023,35.1307568986686,25.5));
#124619=CARTESIAN_POINT('',(-16.5083933915038,35.1310458309266,26.));
#124620=CARTESIAN_POINT('',(-16.5083755433052,35.631045830608,25.5));
#124621=CARTESIAN_POINT('Origin',(-16.5083933915038,35.1310458309266,25.5));
#124622=CARTESIAN_POINT('',(-8.41421811483168,35.6307568983501,25.5));
#124623=CARTESIAN_POINT('',(-8.41423596303023,35.1307568986686,26.));
#124624=CARTESIAN_POINT('Origin',(-16.5083574095355,36.1390458302844,25.5));
#124625=CARTESIAN_POINT('',(-15.5003574101777,36.1390098483161,26.));
#124626=CARTESIAN_POINT('',(-16.0003574098591,36.1390276965147,25.5));
#124627=CARTESIAN_POINT('Origin',(-15.5003574101777,36.1390098483161,25.5));
#124628=CARTESIAN_POINT('Origin',(-16.5083574095355,36.1390458302844,25.5));
#124629=CARTESIAN_POINT('Origin',(-16.5083574095355,36.1390458302844,26.));
#124630=CARTESIAN_POINT('Origin',(-15.5005003304909,32.1352356652978,25.5));
#124631=CARTESIAN_POINT('',(-15.5000542763735,44.6310098429057,26.));
#124632=CARTESIAN_POINT('',(-16.0000542760549,44.6310276911043,25.5));
#124633=CARTESIAN_POINT('Origin',(-15.5000542763735,44.6310098429057,25.5));
#124634=CARTESIAN_POINT('',(-16.0005003301724,32.1352535134963,25.5));
#124635=CARTESIAN_POINT('',(-15.5005003304909,32.1352356652978,26.));
#124636=CARTESIAN_POINT('Origin',(6.40011460523903,44.6304565378295,25.5));
#124637=CARTESIAN_POINT('',(12.8005576038968,45.1304565378295,25.5));
#124638=CARTESIAN_POINT('',(12.8005576038968,44.6304565378295,26.));
#124639=CARTESIAN_POINT('Origin',(12.8005576038968,44.6304565378295,25.5));
#124640=CARTESIAN_POINT('',(6.40011460523903,44.6304565378295,26.));
#124641=CARTESIAN_POINT('',(15.5005576038968,45.1304565378295,25.5));
#124642=CARTESIAN_POINT('Origin',(15.5005576038968,44.6304565378295,25.5));
#124643=CARTESIAN_POINT('',(6.40011460523903,45.1304565378295,25.5));
#124644=CARTESIAN_POINT('Origin',(-6.40003962806013,44.6307992338217,25.5));
#124645=CARTESIAN_POINT('',(-12.8000364298952,45.130913462315,25.5));
#124646=CARTESIAN_POINT('',(-6.40003070396085,45.130799233742,25.5));
#124647=CARTESIAN_POINT('',(-12.8000453539944,44.6309134623946,26.));
#124648=CARTESIAN_POINT('Origin',(-12.8000453539944,44.6309134623946,25.5));
#124649=CARTESIAN_POINT('',(-6.40003962806013,44.6307992338217,26.));
#124650=CARTESIAN_POINT('Origin',(-7.74989684768079,44.6307331902084,25.5));
#124651=CARTESIAN_POINT('',(-15.5000364281749,45.1310098425872,25.5));
#124652=CARTESIAN_POINT('',(-7.74987899948224,45.1307331898898,25.5));
#124653=CARTESIAN_POINT('Origin',(-15.5000542763735,44.6310098429057,25.5));
#124654=CARTESIAN_POINT('',(-7.74989684768079,44.6307331902084,26.));
#124655=CARTESIAN_POINT('Origin',(-15.5000542763735,44.6310098429057,25.5));
#124656=CARTESIAN_POINT('Origin',(-15.5000542763735,44.6310098429057,25.5));
#124657=CARTESIAN_POINT('Origin',(15.5005576038968,44.6304565378295,25.5));
#124658=CARTESIAN_POINT('Origin',(15.5005576038968,44.6304565378295,25.5));
#124659=CARTESIAN_POINT('Origin',(-15.7502284469069,24.1310622223319,26.));
#124660=CARTESIAN_POINT('',(-18.4697586471852,22.6851868854601,12.5));
#124661=CARTESIAN_POINT('',(-18.4697586471852,22.6851868854601,26.));
#124662=CARTESIAN_POINT('',(-15.7502284469069,24.1310622223319,12.5));
#124663=CARTESIAN_POINT('',(-8.78174658325559,27.8359506847069,12.5));
#124664=CARTESIAN_POINT('',(-15.7502284469069,24.1310622223319,26.));
#124665=CARTESIAN_POINT('Origin',(-18.0003186027463,21.8022225347204,26.));
#124666=CARTESIAN_POINT('',(-19.0003186021092,21.8022582311175,12.5));
#124667=CARTESIAN_POINT('',(-19.0003186021092,21.8022582311175,26.));
#124668=CARTESIAN_POINT('Origin',(-18.0003186027463,21.8022225347204,12.5));
#124669=CARTESIAN_POINT('Origin',(-19.0003186021092,21.8022582311175,26.));
#124670=CARTESIAN_POINT('',(-19.000645973767,12.6312582369605,12.5));
#124671=CARTESIAN_POINT('',(-19.000645973767,12.6312582369605,26.));
#124672=CARTESIAN_POINT('',(-19.0002056350033,24.9669223155665,12.5));
#124673=CARTESIAN_POINT('Origin',(-19.000645973767,12.6312582369605,26.));
#124674=CARTESIAN_POINT('',(-20.500472992218,11.1315382915292,12.5));
#124675=CARTESIAN_POINT('',(-20.500472992218,11.1315382915292,26.));
#124676=CARTESIAN_POINT('',(-10.3753149821335,21.2559734640938,12.5));
#124677=CARTESIAN_POINT('Origin',(-20.500472992218,11.1315382915292,26.));
#124678=CARTESIAN_POINT('',(-25.0004729893509,11.1316989253161,12.5));
#124679=CARTESIAN_POINT('',(-25.0004729893509,11.1316989253161,26.));
#124680=CARTESIAN_POINT('',(-10.2507041140081,11.1311724117089,12.5));
#124681=CARTESIAN_POINT('Origin',(-25.0004372929538,12.131698924679,26.));
#124682=CARTESIAN_POINT('',(-26.0004372923167,12.1317346210761,12.5));
#124683=CARTESIAN_POINT('',(-26.0004372923167,12.1317346210761,26.));
#124684=CARTESIAN_POINT('Origin',(-25.0004372929538,12.131698924679,12.5));
#124685=CARTESIAN_POINT('Origin',(-26.0004372923167,12.1317346210761,26.));
#124686=CARTESIAN_POINT('',(-25.9999553909559,25.631734612475,12.5));
#124687=CARTESIAN_POINT('',(-25.9999553909559,25.631734612475,26.));
#124688=CARTESIAN_POINT('',(-26.0001517193255,20.1317854438928,12.5));
#124689=CARTESIAN_POINT('Origin',(-20.9999553941414,25.6315561304895,26.));
#124690=CARTESIAN_POINT('',(-24.5353630919994,29.167216239992,12.5));
#124691=CARTESIAN_POINT('',(-24.5353630919994,29.167216239992,26.));
#124692=CARTESIAN_POINT('Origin',(-20.9999553941414,25.6315561304895,12.5));
#124693=CARTESIAN_POINT('Origin',(-24.5353630919994,29.167216239992,26.));
#124694=CARTESIAN_POINT('',(-18.9497272510074,34.7524533210679,12.5));
#124695=CARTESIAN_POINT('',(-18.9497272510074,34.7524533210679,26.));
#124696=CARTESIAN_POINT('',(-18.6602435263003,35.0419163794607,12.5));
#124697=CARTESIAN_POINT('Origin',(-16.8284826322926,32.6310572553665,26.));
#124698=CARTESIAN_POINT('',(-16.8283755431013,35.6310572534551,15.));
#124699=CARTESIAN_POINT('',(-16.8283755431013,35.6310572534551,26.));
#124700=CARTESIAN_POINT('',(-18.7486119524321,34.9360742604969,15.));
#124701=CARTESIAN_POINT('Origin',(-16.8284826322926,32.6310572553665,15.));
#124702=CARTESIAN_POINT('',(-18.7486119524321,34.9360742604969,12.5));
#124703=CARTESIAN_POINT('',(-18.7486119524321,34.9360742604969,12.));
#124704=CARTESIAN_POINT('Origin',(-16.8284826322926,32.6310572553665,12.5));
#124705=CARTESIAN_POINT('Origin',(-16.8283755431013,35.6310572534551,26.));
#124706=CARTESIAN_POINT('',(-16.5083755433052,35.631045830608,15.));
#124707=CARTESIAN_POINT('',(-16.5083755433052,35.631045830608,26.));
#124708=CARTESIAN_POINT('',(-16.3514391790885,35.6310402285453,15.));
#124709=CARTESIAN_POINT('Origin',(-16.5083574095355,36.1390458302844,26.));
#124710=CARTESIAN_POINT('',(-16.0003574098591,36.1390276965147,15.));
#124711=CARTESIAN_POINT('',(-16.0003574098591,36.1390276965147,26.));
#124712=CARTESIAN_POINT('Origin',(-16.5083574095355,36.1390458302844,15.));
#124713=CARTESIAN_POINT('Origin',(-16.0003574098591,36.1390276965147,26.));
#124714=CARTESIAN_POINT('',(-16.0000542760549,44.6310276911043,12.5));
#124715=CARTESIAN_POINT('',(-16.0000542760549,44.6310276911043,26.));
#124716=CARTESIAN_POINT('',(-16.0002503206678,39.1390276946033,12.5));
#124717=CARTESIAN_POINT('',(-16.0005003301724,32.1352535134963,12.5));
#124718=CARTESIAN_POINT('',(-16.0002503206678,39.1390276946033,15.));
#124719=CARTESIAN_POINT('',(-16.0002503206678,39.1390276946033,12.));
#124720=CARTESIAN_POINT('',(-16.0003574097789,36.1390299426383,15.));
#124721=CARTESIAN_POINT('Origin',(-15.5000542763735,44.6310098429057,26.));
#124722=CARTESIAN_POINT('',(-15.5000364281749,45.1310098425872,12.5));
#124723=CARTESIAN_POINT('',(-15.5000364281749,45.1310098425872,26.));
#124724=CARTESIAN_POINT('Origin',(-15.5000542763735,44.6310098429057,12.5));
#124725=CARTESIAN_POINT('Origin',(-15.5000364281749,45.1310098425872,26.));
#124726=CARTESIAN_POINT('',(-12.8000364298952,45.130913462315,12.5));
#124727=CARTESIAN_POINT('',(-12.8000364298952,45.130913462315,26.));
#124728=CARTESIAN_POINT('',(-7.74987899948224,45.1307331898898,12.5));
#124729=CARTESIAN_POINT('Origin',(-12.8000364298952,45.130913462315,26.));
#124730=CARTESIAN_POINT('',(12.8005576038968,45.1304565378295,12.5));
#124731=CARTESIAN_POINT('',(12.8005576038968,45.1304565378295,26.));
#124732=CARTESIAN_POINT('',(-6.40003070396085,45.130799233742,12.5));
#124733=CARTESIAN_POINT('Origin',(12.8005576038968,45.1304565378295,26.));
#124734=CARTESIAN_POINT('',(15.5005576038968,45.1304565378295,12.5));
#124735=CARTESIAN_POINT('',(15.5005576038968,45.1304565378295,26.));
#124736=CARTESIAN_POINT('',(6.40011460523903,45.1304565378295,12.5));
#124737=CARTESIAN_POINT('Origin',(-0.000328393418778106,28.1309081768848,
26.));
#124738=CARTESIAN_POINT('Origin',(-15.5005003304909,32.1352356652978,12.5));
#124739=CARTESIAN_POINT('',(-15.5000542763735,44.6310098429057,12.));
#124740=CARTESIAN_POINT('Origin',(-15.5000542763735,44.6310098429057,12.5));
#124741=CARTESIAN_POINT('',(-15.5002337542308,39.6031114612468,12.));
#124742=CARTESIAN_POINT('',(-15.5005003304909,32.1352356652978,12.));
#124743=CARTESIAN_POINT('Ctrl Pts',(-15.5002337542308,39.6031114612469,
12.));
#124744=CARTESIAN_POINT('Ctrl Pts',(-15.5012802807782,39.6022052080442,
12.));
#124745=CARTESIAN_POINT('Ctrl Pts',(-15.5023266329781,39.6012987501675,
12.0000032854501));
#124746=CARTESIAN_POINT('Ctrl Pts',(-15.5262620426631,39.580555287795,12.0001535475902));
#124747=CARTESIAN_POINT('Ctrl Pts',(-15.549079071856,39.5606097425883,12.0018685097915));
#124748=CARTESIAN_POINT('Ctrl Pts',(-15.6555915595815,39.4666813170044,
12.0172417791965));
#124749=CARTESIAN_POINT('Ctrl Pts',(-15.7342867260662,39.3947272458287,
12.0503680939609));
#124750=CARTESIAN_POINT('Ctrl Pts',(-15.8544463319837,39.2818437637677,
12.1407858340455));
#124751=CARTESIAN_POINT('Ctrl Pts',(-15.8992348499764,39.2385644267119,
12.1913094880828));
#124752=CARTESIAN_POINT('Ctrl Pts',(-15.9582815856617,39.1808059783461,
12.2931553699351));
#124753=CARTESIAN_POINT('Ctrl Pts',(-15.9780823063818,39.1611342110301,
12.3427321807669));
#124754=CARTESIAN_POINT('Ctrl Pts',(-15.996608615715,39.1426753037105,12.4305871755406));
#124755=CARTESIAN_POINT('Ctrl Pts',(-16.0002503206678,39.1390276946034,
12.4651445835938));
#124756=CARTESIAN_POINT('Ctrl Pts',(-16.0002503206678,39.1390276946034,
12.5));
#124757=CARTESIAN_POINT('Origin',(-16.0003574098591,36.1390276965147,12.5));
#124758=CARTESIAN_POINT('',(-18.8658210632966,34.1292719773217,12.));
#124759=CARTESIAN_POINT('Origin',(-16.0003574098591,36.1390276965147,12.));
#124760=CARTESIAN_POINT('',(-18.810086036752,34.6128021370802,12.1018952060707));
#124761=CARTESIAN_POINT('Ctrl Pts',(-18.8658210632966,34.1292719773218,
12.));
#124762=CARTESIAN_POINT('Ctrl Pts',(-18.8656807480304,34.1308827000774,
12.));
#124763=CARTESIAN_POINT('Ctrl Pts',(-18.8655400049988,34.1324933903515,
12.0000032434225));
#124764=CARTESIAN_POINT('Ctrl Pts',(-18.8573778375603,34.2256175041316,
12.0003779495169));
#124765=CARTESIAN_POINT('Ctrl Pts',(-18.8478563981534,34.3178692956092,
12.0111952320961));
#124766=CARTESIAN_POINT('Ctrl Pts',(-18.8288764025859,34.4771426650498,
12.048491997422));
#124767=CARTESIAN_POINT('Ctrl Pts',(-18.8196146553393,34.5470501977567,
12.0716841972469));
#124768=CARTESIAN_POINT('Ctrl Pts',(-18.810086036752,34.6128021370802,12.1018952060707));
#124769=CARTESIAN_POINT('Ctrl Pts',(-18.810086036752,34.6128021370802,12.1018952060707));
#124770=CARTESIAN_POINT('Ctrl Pts',(-18.8089992232141,34.6203016604522,
12.1053410081124));
#124771=CARTESIAN_POINT('Ctrl Pts',(-18.8078973392296,34.6277440210717,
12.1088851897267));
#124772=CARTESIAN_POINT('Ctrl Pts',(-18.7957307106799,34.7082643255815,
12.1486504715915));
#124773=CARTESIAN_POINT('Ctrl Pts',(-18.784159852527,34.7702166242448,12.1921413513201));
#124774=CARTESIAN_POINT('Ctrl Pts',(-18.7672884639414,34.8535445163286,
12.2764946297254));
#124775=CARTESIAN_POINT('Ctrl Pts',(-18.7606689443804,34.8835886882299,
12.3169287768681));
#124776=CARTESIAN_POINT('Ctrl Pts',(-18.7520329511296,34.9216311139679,
12.3986190308673));
#124777=CARTESIAN_POINT('Ctrl Pts',(-18.7494922500063,34.9323419849364,
12.4373510176214));
#124778=CARTESIAN_POINT('Ctrl Pts',(-18.7486753311664,34.9358059214554,
12.4851148185871));
#124779=CARTESIAN_POINT('Ctrl Pts',(-18.7486119524321,34.936074260497,12.4925693313125));
#124780=CARTESIAN_POINT('Ctrl Pts',(-18.7486119524321,34.936074260497,12.5));
#124781=CARTESIAN_POINT('Origin',(-16.0003574098591,36.1390276965147,12.5));
#124782=CARTESIAN_POINT('Origin',(-7.74989684768079,44.6307331902083,12.5));
#124783=CARTESIAN_POINT('',(-12.8000542780937,44.6309134626335,12.));
#124784=CARTESIAN_POINT('Origin',(-12.8000542780937,44.6309134626335,12.5));
#124785=CARTESIAN_POINT('',(-7.74989684768079,44.6307331902083,12.));
#124786=CARTESIAN_POINT('Origin',(-15.5000542763735,44.6310098429057,12.5));
#124787=CARTESIAN_POINT('Origin',(-6.40003962806013,44.6307992338217,12.5));
#124788=CARTESIAN_POINT('',(12.8005486797976,44.6304565379091,12.));
#124789=CARTESIAN_POINT('Origin',(12.8005486797976,44.6304565379091,12.5));
#124790=CARTESIAN_POINT('',(-6.40003962806013,44.6307992338217,12.));
#124791=CARTESIAN_POINT('Origin',(6.40011460523903,44.6304565378295,12.5));
#124792=CARTESIAN_POINT('',(15.5005576038968,44.6304565378295,12.));
#124793=CARTESIAN_POINT('Origin',(15.5005576038968,44.6304565378295,12.5));
#124794=CARTESIAN_POINT('',(6.40011460523903,44.6304565378295,12.));
#124795=CARTESIAN_POINT('Origin',(-15.5000542763735,44.6310098429057,12.5));
#124796=CARTESIAN_POINT('Origin',(16.0005576038968,36.1384565378295,12.5));
#124797=CARTESIAN_POINT('',(16.0005576038968,39.1384565378295,12.5));
#124798=CARTESIAN_POINT('',(18.7487692036153,34.9354049997927,12.5));
#124799=CARTESIAN_POINT('Origin',(16.0005576038968,36.1384565378295,12.5));
#124800=CARTESIAN_POINT('',(18.8102317482459,34.6121306821786,12.1018952060707));
#124801=CARTESIAN_POINT('Ctrl Pts',(18.7487692036153,34.9354049997927,12.5));
#124802=CARTESIAN_POINT('Ctrl Pts',(18.7487692036153,34.9354049997927,12.4925693313125));
#124803=CARTESIAN_POINT('Ctrl Pts',(18.7488325727708,34.9351366584889,12.4851148185871));
#124804=CARTESIAN_POINT('Ctrl Pts',(18.7496493679601,34.9316726928111,12.4373510176214));
#124805=CARTESIAN_POINT('Ctrl Pts',(18.7521896867423,34.9209617311555,12.3986190308672));
#124806=CARTESIAN_POINT('Ctrl Pts',(18.7608243220101,34.8829189971679,12.3169287768681));
#124807=CARTESIAN_POINT('Ctrl Pts',(18.7674427690982,34.8528745889928,12.2764946297254));
#124808=CARTESIAN_POINT('Ctrl Pts',(18.7843111831675,34.7695460947143,12.1921413513201));
#124809=CARTESIAN_POINT('Ctrl Pts',(18.7958798298391,34.7075933830526,12.1486504715916));
#124810=CARTESIAN_POINT('Ctrl Pts',(18.8080435840964,34.6270726442891,12.1088851897267));
#124811=CARTESIAN_POINT('Ctrl Pts',(18.8091452024147,34.6196302443412,12.1053410081124));
#124812=CARTESIAN_POINT('Ctrl Pts',(18.8102317482459,34.6121306821786,12.1018952060707));
#124813=CARTESIAN_POINT('',(18.8659495144705,34.1285985331886,12.));
#124814=CARTESIAN_POINT('Ctrl Pts',(18.8102317482459,34.6121306821786,12.1018952060707));
#124815=CARTESIAN_POINT('Ctrl Pts',(18.8197580197198,34.5463784027596,12.0716841972469));
#124816=CARTESIAN_POINT('Ctrl Pts',(18.8290172715136,34.4764705394863,12.048491997422));
#124817=CARTESIAN_POINT('Ctrl Pts',(18.8479915815834,34.31719649263,12.0111952320961));
#124818=CARTESIAN_POINT('Ctrl Pts',(18.8575097279275,34.2249443613316,12.0003779495169));
#124819=CARTESIAN_POINT('Ctrl Pts',(18.8656685711657,34.1318199562489,12.0000032434225));
#124820=CARTESIAN_POINT('Ctrl Pts',(18.8658092567013,34.1302092609521,12.));
#124821=CARTESIAN_POINT('Ctrl Pts',(18.8659495144705,34.1285985331886,12.));
#124822=CARTESIAN_POINT('',(15.5005576038968,39.6025581529673,12.));
#124823=CARTESIAN_POINT('Origin',(16.0005576038968,36.1384565378295,12.));
#124824=CARTESIAN_POINT('Ctrl Pts',(15.5005576038968,39.6025581529673,12.));
#124825=CARTESIAN_POINT('Ctrl Pts',(15.5016040980935,39.601651862408,12.));
#124826=CARTESIAN_POINT('Ctrl Pts',(15.5026504179355,39.6007453671807,12.0000032854501));
#124827=CARTESIAN_POINT('Ctrl Pts',(15.5265850871382,39.5800010504138,12.0001535475902));
#124828=CARTESIAN_POINT('Ctrl Pts',(15.5494014043324,39.5600546907341,12.0018685097915));
#124829=CARTESIAN_POINT('Ctrl Pts',(15.6559105390839,39.4661224630977,12.0172417791965));
#124830=CARTESIAN_POINT('Ctrl Pts',(15.7346031370174,39.394165582834,12.050368093961));
#124831=CARTESIAN_POINT('Ctrl Pts',(15.8547587133248,39.2812778115798,12.1407858340455));
#124832=CARTESIAN_POINT('Ctrl Pts',(15.8995456863726,39.2379968757629,12.1913094880829));
#124833=CARTESIAN_POINT('Ctrl Pts',(15.9585903602516,39.1802363196783,12.2931553699351));
#124834=CARTESIAN_POINT('Ctrl Pts',(15.9783903787479,39.1605638455604,12.3427321807669));
#124835=CARTESIAN_POINT('Ctrl Pts',(15.9969160291529,39.1421042769301,12.4305871755405));
#124836=CARTESIAN_POINT('Ctrl Pts',(16.0005576038968,39.1384565378295,12.4651445835938));
#124837=CARTESIAN_POINT('Ctrl Pts',(16.0005576038968,39.1384565378295,12.5));
#124838=CARTESIAN_POINT('Origin',(15.5005576038968,36.3806823573572,12.5));
#124839=CARTESIAN_POINT('',(15.5005576038968,36.3806823573572,12.));
#124840=CARTESIAN_POINT('',(16.0005576038968,44.6304565378295,12.5));
#124841=CARTESIAN_POINT('Origin',(15.5005576038968,44.6304565378295,12.5));
#124842=CARTESIAN_POINT('',(16.0005576038968,36.3806823573572,12.5));
#124843=CARTESIAN_POINT('Origin',(15.5005576038968,44.6304565378295,12.5));
#124844=CARTESIAN_POINT('Origin',(15.5005576038968,44.6304565378295,12.5));
#124845=CARTESIAN_POINT('Origin',(-18.3067027565145,34.6883503685105,12.5));
#124846=CARTESIAN_POINT('',(-24.1818223222136,28.8136502290417,12.));
#124847=CARTESIAN_POINT('',(-18.3067027565145,34.6883503685105,12.));
#124848=CARTESIAN_POINT('Origin',(-24.1818223222136,28.8136502290417,12.5));
#124849=CARTESIAN_POINT('Origin',(-18.5961864812216,34.3988873101177,12.5));
#124850=CARTESIAN_POINT('Origin',(-0.000328393418778106,28.1309081768848,
12.));
#124851=CARTESIAN_POINT('',(24.1817610214557,28.8127870262033,12.));
#124852=CARTESIAN_POINT('',(15.5139901477705,37.4805578998886,12.));
#124853=CARTESIAN_POINT('',(25.4997805061163,25.6308065108639,12.));
#124854=CARTESIAN_POINT('Origin',(20.9997805061163,25.6308065108639,12.));
#124855=CARTESIAN_POINT('',(25.4997805061163,12.1308065108639,12.));
#124856=CARTESIAN_POINT('',(25.4997805061163,26.8808573438743,12.));
#124857=CARTESIAN_POINT('',(24.9997805061163,11.6308065108639,12.));
#124858=CARTESIAN_POINT('Origin',(24.9997805061163,12.1308065108639,12.));
#124859=CARTESIAN_POINT('',(20.7068872873028,11.6308065108639,12.));
#124860=CARTESIAN_POINT('',(12.4997260563488,11.6308065108639,12.));
#124861=CARTESIAN_POINT('',(19.5000070232196,12.8376867749471,12.));
#124862=CARTESIAN_POINT('',(11.4782812553205,20.8594125428461,12.));
#124863=CARTESIAN_POINT('',(19.5000070232196,21.8015799937605,12.));
#124864=CARTESIAN_POINT('',(19.5000070232196,20.3807440853227,12.));
#124865=CARTESIAN_POINT('',(18.7042143673984,23.1260013830489,12.));
#124866=CARTESIAN_POINT('Origin',(18.0000070232196,21.8015799937605,12.));
#124867=CARTESIAN_POINT('',(15.8746640014216,24.6305,12.));
#124868=CARTESIAN_POINT('',(10.3759028387591,27.5542431726415,12.));
#124869=CARTESIAN_POINT('',(12.,24.6305,12.));
#124870=CARTESIAN_POINT('',(7.87483580329061,24.6305,12.));
#124871=CARTESIAN_POINT('',(-12.0002195251968,24.6309283607631,12.));
#124872=CARTESIAN_POINT('',(5.99980902926158,24.6306070926795,12.));
#124873=CARTESIAN_POINT('',(-15.8748746000505,24.631066672069,12.));
#124874=CARTESIAN_POINT('',(-6.00033197323811,24.630714186474,12.));
#124875=CARTESIAN_POINT('',(-18.7044786694047,23.12666906083,12.));
#124876=CARTESIAN_POINT('',(-9.01646660547503,28.2774328600768,12.));
#124877=CARTESIAN_POINT('',(-19.5003186017906,21.8022760793161,12.));
#124878=CARTESIAN_POINT('Origin',(-18.0003186027463,21.8022225347204,12.));
#124879=CARTESIAN_POINT('',(-19.5006385804826,12.8383828662136,12.));
#124880=CARTESIAN_POINT('',(-19.5002056346847,24.9669401637651,12.));
#124881=CARTESIAN_POINT('',(-20.707561925074,11.6315456841765,12.));
#124882=CARTESIAN_POINT('',(-10.7288557519193,21.609539475044,12.));
#124883=CARTESIAN_POINT('',(-25.0004551411524,11.6316989249976,12.));
#124884=CARTESIAN_POINT('',(-10.2506862658096,11.6311724113903,12.));
#124885=CARTESIAN_POINT('',(-25.5004372926353,12.1317167728775,12.));
#124886=CARTESIAN_POINT('Origin',(-25.0004372929538,12.131698924679,12.));
#124887=CARTESIAN_POINT('',(-25.4999553912744,25.6317167642765,12.));
#124888=CARTESIAN_POINT('',(-25.5001517196441,20.1317675956942,12.));
#124889=CARTESIAN_POINT('Origin',(-20.9999553941414,25.6315561304895,12.));
#124890=CARTESIAN_POINT('Origin',(15.5139901477705,37.4805578998886,12.5));
#124891=CARTESIAN_POINT('',(18.9498779474565,34.7517768813891,12.5));
#124892=CARTESIAN_POINT('Origin',(18.5963245568632,34.3982234907959,12.5));
#124893=CARTESIAN_POINT('',(24.535314412049,29.1663404167966,12.5));
#124894=CARTESIAN_POINT('',(15.8675435383638,37.8341112904819,12.5));
#124895=CARTESIAN_POINT('Origin',(24.1817610214557,28.8127870262033,12.5));
#124896=CARTESIAN_POINT('Origin',(16.8285576038968,32.6304565378295,12.5));
#124897=CARTESIAN_POINT('Origin',(16.8285576038968,32.6304565378295,12.5));
#124898=CARTESIAN_POINT('Origin',(-10.2506862658096,11.6311724113903,12.5));
#124899=CARTESIAN_POINT('Origin',(-25.0004551411524,11.6316989249976,12.5));
#124900=CARTESIAN_POINT('Origin',(-20.707561925074,11.6315456841765,12.5));
#124901=CARTESIAN_POINT('Ctrl Pts',(-25.0004729893509,11.1316989253161,
12.5000000000001));
#124902=CARTESIAN_POINT('Ctrl Pts',(-26.0004729887137,11.1317346217133,
12.5000000000001));
#124903=CARTESIAN_POINT('Ctrl Pts',(-26.0004372923167,12.1317346210761,
12.5));
#124904=CARTESIAN_POINT('Ctrl Pts',(-25.0004729893509,11.131698925316,11.9999999999999));
#124905=CARTESIAN_POINT('Ctrl Pts',(-26.0004729887137,11.1317346217132,
12.));
#124906=CARTESIAN_POINT('Ctrl Pts',(-26.0004372923168,12.131734621076,11.9999999999999));
#124907=CARTESIAN_POINT('Ctrl Pts',(-25.0004551411523,11.6316989249976,
12.));
#124908=CARTESIAN_POINT('Ctrl Pts',(-25.5004551408337,11.6317167731962,
12.));
#124909=CARTESIAN_POINT('Ctrl Pts',(-25.5004372926352,12.1317167728776,
12.));
#124910=CARTESIAN_POINT('Origin',(-25.5004372926353,12.1317167728775,12.5));
#124911=CARTESIAN_POINT('Origin',(-25.5001517196441,20.1317675956942,12.5));
#124912=CARTESIAN_POINT('Origin',(-25.4999553912744,25.6317167642765,12.5));
#124913=CARTESIAN_POINT('Origin',(-20.9999553941414,25.6315561304895,12.5));
#124914=CARTESIAN_POINT('Origin',(-16.8284826322926,32.6310572553665,12.5));
#124915=CARTESIAN_POINT('Origin',(-10.7288557519193,21.609539475044,12.5));
#124916=CARTESIAN_POINT('Origin',(-19.5006385804826,12.8383828662136,12.5));
#124917=CARTESIAN_POINT('Origin',(-9.01646660547503,28.2774328600768,12.5));
#124918=CARTESIAN_POINT('Origin',(-18.7044786694047,23.12666906083,12.5));
#124919=CARTESIAN_POINT('Origin',(-15.8748746000505,24.631066672069,12.5));
#124920=CARTESIAN_POINT('Origin',(-18.0003186027463,21.8022225347204,12.5));
#124921=CARTESIAN_POINT('Origin',(-19.5003186017906,21.8022760793161,12.5));
#124922=CARTESIAN_POINT('Origin',(-19.5002056346847,24.9669401637651,12.5));
#124923=CARTESIAN_POINT('Origin',(7.87483580329061,24.6305,12.5));
#124924=CARTESIAN_POINT('',(15.75,24.1305,12.5));
#124925=CARTESIAN_POINT('',(12.,24.1305,12.5));
#124926=CARTESIAN_POINT('',(7.87483580329061,24.1305,12.5));
#124927=CARTESIAN_POINT('Origin',(12.,24.6305,12.5));
#124928=CARTESIAN_POINT('Origin',(15.8746640014216,24.6305,12.5));
#124929=CARTESIAN_POINT('Origin',(5.99980902926158,24.6306070926795,12.5));
#124930=CARTESIAN_POINT('',(-12.0002284492961,24.1309283608428,12.5));
#124931=CARTESIAN_POINT('Origin',(-12.0002195251968,24.6309283607631,12.5));
#124932=CARTESIAN_POINT('',(5.9998001051623,24.1306070927591,12.5));
#124933=CARTESIAN_POINT('Origin',(-6.00033197323811,24.630714186474,12.5));
#124934=CARTESIAN_POINT('',(-6.00034982143666,24.1307141867926,12.5));
#124935=CARTESIAN_POINT('Origin',(19.5000070232196,20.3807440853227,12.5));
#124936=CARTESIAN_POINT('',(19.0000070232196,12.6305799937605,12.5));
#124937=CARTESIAN_POINT('',(19.0000070232196,21.8015799937605,12.5));
#124938=CARTESIAN_POINT('',(19.0000070232196,20.3807440853227,12.5));
#124939=CARTESIAN_POINT('Origin',(19.5000070232196,21.8015799937605,12.5));
#124940=CARTESIAN_POINT('Origin',(19.5000070232196,12.8376867749471,12.5));
#124941=CARTESIAN_POINT('Origin',(18.0000070232196,21.8015799937605,12.5));
#124942=CARTESIAN_POINT('',(18.4694785860055,22.6845275866195,12.5));
#124943=CARTESIAN_POINT('Origin',(18.7042143673984,23.1260013830489,12.5));
#124944=CARTESIAN_POINT('Origin',(18.0000070232196,21.8015799937605,12.5));
#124945=CARTESIAN_POINT('Origin',(10.3759028387591,27.5542431726415,12.5));
#124946=CARTESIAN_POINT('',(10.1411670573662,27.112769376212,12.5));
#124947=CARTESIAN_POINT('Origin',(11.4782812553205,20.8594125428461,12.5));
#124948=CARTESIAN_POINT('',(20.4997805061163,11.1308065108639,12.5));
#124949=CARTESIAN_POINT('',(11.1247278647273,20.5058591522529,12.5));
#124950=CARTESIAN_POINT('Origin',(20.7068872873028,11.6308065108639,12.5));
#124951=CARTESIAN_POINT('Origin',(20.9997805061163,25.6308065108639,12.5));
#124952=CARTESIAN_POINT('',(25.9997805061163,25.6308065108639,12.5));
#124953=CARTESIAN_POINT('Origin',(25.4997805061163,25.6308065108639,12.5));
#124954=CARTESIAN_POINT('Origin',(20.9997805061163,25.6308065108639,12.5));
#124955=CARTESIAN_POINT('Origin',(25.4997805061163,26.8808573438743,12.5));
#124956=CARTESIAN_POINT('',(25.9997805061163,12.1308065108639,12.5));
#124957=CARTESIAN_POINT('Origin',(25.4997805061163,12.1308065108639,12.5));
#124958=CARTESIAN_POINT('',(25.9997805061163,26.8808573438743,12.5));
#124959=CARTESIAN_POINT('Ctrl Pts',(25.9997805061163,12.1308065108639,12.5));
#124960=CARTESIAN_POINT('Ctrl Pts',(25.9997805061163,11.1308065108639,12.5));
#124961=CARTESIAN_POINT('Ctrl Pts',(24.9997805061163,11.1308065108639,12.5));
#124962=CARTESIAN_POINT('Ctrl Pts',(25.9997805061163,12.1308065108639,12.));
#124963=CARTESIAN_POINT('Ctrl Pts',(25.9997805061163,11.1308065108639,12.));
#124964=CARTESIAN_POINT('Ctrl Pts',(24.9997805061163,11.1308065108639,12.));
#124965=CARTESIAN_POINT('Ctrl Pts',(25.4997805061163,12.1308065108639,12.));
#124966=CARTESIAN_POINT('Ctrl Pts',(25.4997805061163,11.6308065108639,12.));
#124967=CARTESIAN_POINT('Ctrl Pts',(24.9997805061163,11.6308065108639,12.));
#124968=CARTESIAN_POINT('',(24.9997805061163,11.1308065108639,12.5));
#124969=CARTESIAN_POINT('Origin',(24.9997805061163,11.6308065108639,12.5));
#124970=CARTESIAN_POINT('Origin',(24.9997805061163,12.1308065108639,12.5));
#124971=CARTESIAN_POINT('Origin',(12.4997260563488,11.6308065108639,12.5));
#124972=CARTESIAN_POINT('',(12.4997260563488,11.1308065108639,12.5));
#124973=CARTESIAN_POINT('Origin',(-12.0002284492961,24.1309283608428,26.));
#124974=CARTESIAN_POINT('',(-12.0002284492961,24.1309283608428,26.));
#124975=CARTESIAN_POINT('Origin',(12.,24.1305,26.));
#124976=CARTESIAN_POINT('',(12.,24.1305,26.));
#124977=CARTESIAN_POINT('Origin',(15.75,24.1305,26.));
#124978=CARTESIAN_POINT('',(15.75,24.1305,26.));
#124979=CARTESIAN_POINT('Origin',(18.4694785860055,22.6845275866195,26.));
#124980=CARTESIAN_POINT('',(18.4694785860055,22.6845275866195,26.));
#124981=CARTESIAN_POINT('Origin',(18.0000070232196,21.8015799937605,26.));
#124982=CARTESIAN_POINT('',(19.0000070232196,21.8015799937605,26.));
#124983=CARTESIAN_POINT('Origin',(19.0000070232196,12.6305799937605,26.));
#124984=CARTESIAN_POINT('',(19.0000070232196,12.6305799937605,26.));
#124985=CARTESIAN_POINT('Origin',(20.4997805061163,11.1308065108639,26.));
#124986=CARTESIAN_POINT('',(20.4997805061163,11.1308065108639,26.));
#124987=CARTESIAN_POINT('Origin',(24.9997805061163,11.1308065108639,26.));
#124988=CARTESIAN_POINT('',(24.9997805061163,11.1308065108639,26.));
#124989=CARTESIAN_POINT('Origin',(24.9997805061163,12.1308065108639,26.));
#124990=CARTESIAN_POINT('',(25.9997805061163,12.1308065108639,26.));
#124991=CARTESIAN_POINT('Origin',(25.9997805061163,25.6308065108639,26.));
#124992=CARTESIAN_POINT('',(25.9997805061163,25.6308065108639,26.));
#124993=CARTESIAN_POINT('Origin',(20.9997805061163,25.6308065108639,26.));
#124994=CARTESIAN_POINT('',(24.535314412049,29.1663404167966,26.));
#124995=CARTESIAN_POINT('Origin',(18.9498779474565,34.7517768813891,26.));
#124996=CARTESIAN_POINT('',(18.9498779474565,34.7517768813891,26.));
#124997=CARTESIAN_POINT('Origin',(16.8285576038968,32.6304565378295,26.));
#124998=CARTESIAN_POINT('',(18.7487692036153,34.9354049997927,15.));
#124999=CARTESIAN_POINT('',(18.7487692036153,34.9354049997927,12.));
#125000=CARTESIAN_POINT('',(16.8285576038968,35.6304565378295,15.));
#125001=CARTESIAN_POINT('Origin',(16.8285576038968,32.6304565378295,15.));
#125002=CARTESIAN_POINT('',(16.8285576038968,35.6304565378295,26.));
#125003=CARTESIAN_POINT('Origin',(16.0005576038968,36.1384565378295,12.));
#125004=CARTESIAN_POINT('',(16.0005576038968,39.1384565378295,15.));
#125005=CARTESIAN_POINT('',(16.0005576038968,39.1384565378295,12.));
#125006=CARTESIAN_POINT('Origin',(16.0005576038968,36.1384565378295,15.));
#125007=CARTESIAN_POINT('Origin',(-16.0003574098591,36.1390276965147,12.));
#125008=CARTESIAN_POINT('Origin',(-16.0003574098591,36.1390276965147,15.));
#125009=CARTESIAN_POINT('Origin',(-15.8744846811456,36.139027695559,15.));
#125010=CARTESIAN_POINT('Origin',(15.8746634037561,36.1384565378295,15.));
#125011=CARTESIAN_POINT('',(16.5085576038968,35.6304565378295,15.));
#125012=CARTESIAN_POINT('',(16.1916105038265,35.6304565378295,15.));
#125013=CARTESIAN_POINT('',(16.0005576038968,36.1384565378295,15.));
#125014=CARTESIAN_POINT('',(16.0005576038968,40.3844565378295,15.));
#125015=CARTESIAN_POINT('Origin',(16.5085576038968,36.1384565378295,15.));
#125016=CARTESIAN_POINT('Origin',(16.5085576038968,35.6304565378295,26.));
#125017=CARTESIAN_POINT('',(16.5085576038968,35.6304565378295,26.));
#125018=CARTESIAN_POINT('Origin',(16.5085576038968,36.1384565378295,26.));
#125019=CARTESIAN_POINT('',(16.0005576038968,36.1384565378295,26.));
#125020=CARTESIAN_POINT('Origin',(16.0005576038968,44.6304565378295,26.));
#125021=CARTESIAN_POINT('',(16.0005576038968,44.6304565378295,26.));
#125022=CARTESIAN_POINT('Origin',(15.5005576038968,44.6304565378295,26.));
#215593=UNCERTAINTY_MEASURE_WITH_UNIT(LENGTH_MEASURE(0.01),#215610,
'DISTANCE_ACCURACY_VALUE',
'Maximum model space distance between geometric entities at asserted c
onnectivities');
#215598=UNCERTAINTY_MEASURE_WITH_UNIT(LENGTH_MEASURE(0.01),#215610,
'DISTANCE_ACCURACY_VALUE',
'Maximum model space distance between geometric entities at asserted c
onnectivities');
#215604=(
GEOMETRIC_REPRESENTATION_CONTEXT(3)
GLOBAL_UNCERTAINTY_ASSIGNED_CONTEXT((#215593))
GLOBAL_UNIT_ASSIGNED_CONTEXT((#215610,#215612,#215613))
REPRESENTATION_CONTEXT('','3D')
);
#215609=(
GEOMETRIC_REPRESENTATION_CONTEXT(3)
GLOBAL_UNCERTAINTY_ASSIGNED_CONTEXT((#215598))
GLOBAL_UNIT_ASSIGNED_CONTEXT((#215610,#215612,#215613))
REPRESENTATION_CONTEXT('','3D')
);
#215610=(
LENGTH_UNIT()
NAMED_UNIT(*)
SI_UNIT(.MILLI.,.METRE.)
);
#215612=(
NAMED_UNIT(*)
PLANE_ANGLE_UNIT()
SI_UNIT($,.RADIAN.)
);
#215613=(
NAMED_UNIT(*)
SI_UNIT($,.STERADIAN.)
SOLID_ANGLE_UNIT()
);
#215619=SHAPE_DEFINITION_REPRESENTATION(#215629,#215648);
#215629=PRODUCT_DEFINITION_SHAPE('',$,#215659);
#215648=SHAPE_REPRESENTATION('',(#28710),#215604);
#215653=PRODUCT_DEFINITION_CONTEXT('part definition',#215685,'design');
#215659=PRODUCT_DEFINITION('2026-10-04-16-01-39-984','CarregeSupport',#215669,
#215653);
#215669=PRODUCT_DEFINITION_FORMATION('',$,#215692);
#215685=APPLICATION_CONTEXT(
'Core Data for Automotive Mechanical Design Process');
#215686=PRODUCT_CONTEXT('part definition',#215685,'mechanical');
#215692=PRODUCT('2026-10-04-16-01-39-984','CarregeSupport',$,(#215686));
#215698=PRESENTATION_STYLE_ASSIGNMENT((#215700));
#215700=SURFACE_STYLE_USAGE(.BOTH.,#215702);
#215702=SURFACE_SIDE_STYLE('',(#215704));
#215704=SURFACE_STYLE_FILL_AREA(#215706);
#215706=FILL_AREA_STYLE('Opaque(245,245,246)',(#215708));
#215708=FILL_AREA_STYLE_COLOUR('Opaque(245,245,246)',#215710);
#215710=COLOUR_RGB('Opaque(245,245,246)', 0.66274510, 0.83137255, 0.94901961);
ENDSEC;
END-ISO-10303-21;
